ISO-10303-21;
HEADER;
FILE_DESCRIPTION (('STEP AP214'),
    '1' );
FILE_NAME ('Insulating Base Plate.step',
    '2026-10-09T19:32:29',
    ( '' ),
    ( '' ),
    'SwSTEP 2.0',
    'SolidWorks 2026',
    '' );
FILE_SCHEMA (( 'AUTOMOTIVE_DESIGN' ));
ENDSEC;

DATA;
#7=CARTESIAN_POINT ( 'NONE',  ( 0.1749999999999999889, 2.700000000000000178, 0.5999999999999999778 ) ) ;
#13=EDGE_CURVE ( 'NONE', #12197, #10130, #5306, .T. ) ;
#64=DIRECTION ( 'NONE',  ( 1.000000000000000000, 0.000000000000000000, 0.000000000000000000 ) ) ;
#71=LINE ( 'NONE', #1553, #14401 ) ;
#83=DIRECTION ( 'NONE',  ( -1.000000000000000000, 0.000000000000000000, 0.000000000000000000 ) ) ;
#94=LINE ( 'NONE', #11471, #11442 ) ;
#114=DIRECTION ( 'NONE',  ( 0.000000000000000000, -1.000000000000000000, 0.000000000000000000 ) ) ;
#120=DIRECTION ( 'NONE',  ( -0.000000000000000000, 1.000000000000000000, 0.000000000000000000 ) ) ;
#135=VECTOR ( 'NONE', #8879, 1000.000000000000000 ) ;
#149=ORIENTED_EDGE ( 'NONE', *, *, #14001, .F. ) ;
#214=ORIENTED_EDGE ( 'NONE', *, *, #13, .F. ) ;
#225=ORIENTED_EDGE ( 'NONE', *, *, #4277, .F. ) ;
#228=AXIS2_PLACEMENT_3D ( 'NONE', #7610, #10199, #579 ) ;
#249=AXIS2_PLACEMENT_3D ( 'NONE', #9297, #17801, #8028 ) ;
#253=DIRECTION ( 'NONE',  ( -1.000000000000000000, -1.168655815394900078E-16, -2.220446049250309876E-16 ) ) ;
#260=VECTOR ( 'NONE', #17975, 1000.000000000000000 ) ;
#265=DIRECTION ( 'NONE',  ( 0.000000000000000000, 0.000000000000000000, -1.000000000000000000 ) ) ;
#279=VECTOR ( 'NONE', #3953, 1000.000000000000000 ) ;
#288=CARTESIAN_POINT ( 'NONE',  ( -0.1749999999999999889, 5.200000000000000178, 1.600000000000000089 ) ) ;
#302=LINE ( 'NONE', #16960, #1412 ) ;
#309=EDGE_LOOP ( 'NONE', ( #17351, #15970, #6172, #13800, #4182, #16945, #17442, #3306, #8429, #9460, #10234, #6980, #680, #8084, #3687, #8931, #1239, #12150, #7376, #3119, #7225, #7211, #16942, #5389, #10768, #17470, #4563, #16616 ) ) ;
#334=CARTESIAN_POINT ( 'NONE',  ( 1.899999999999999911, 4.700000000000000178, 0.5999999999999999778 ) ) ;
#361=CARTESIAN_POINT ( 'NONE',  ( 1.899999999999999911, 2.799999999999999822, 1.600000000000000089 ) ) ;
#372=EDGE_LOOP ( 'NONE', ( #10666, #14825, #6919, #6474 ) ) ;
#431=FACE_OUTER_BOUND ( 'NONE', #10323, .T. ) ;
#469=VECTOR ( 'NONE', #13422, 1000.000000000000000 ) ;
#476=ORIENTED_EDGE ( 'NONE', *, *, #2348, .F. ) ;
#511=AXIS2_PLACEMENT_3D ( 'NONE', #3068, #18227, #15681 ) ;
#518=DIRECTION ( 'NONE',  ( -2.337311630789800155E-16, 1.000000000000000000, 0.000000000000000000 ) ) ;
#545=DIRECTION ( 'NONE',  ( -4.440892098500630106E-16, 0.000000000000000000, 1.000000000000000000 ) ) ;
#548=FACE_OUTER_BOUND ( 'NONE', #2723, .T. ) ;
#553=ORIENTED_EDGE ( 'NONE', *, *, #10570, .F. ) ;
#558=CARTESIAN_POINT ( 'NONE',  ( -2.500000000000000000, 10.00000000000000000, 1.600000000000000089 ) ) ;
#560=FACE_BOUND ( 'NONE', #795, .T. ) ;
#566=CARTESIAN_POINT ( 'NONE',  ( 2.500000000000000000, 4.700000000000000178, 1.600000000000000089 ) ) ;
#567=DIRECTION ( 'NONE',  ( 0.000000000000000000, 0.000000000000000000, -1.000000000000000000 ) ) ;
#572=AXIS2_PLACEMENT_3D ( 'NONE', #3697, #17666, #14917 ) ;
#579=DIRECTION ( 'NONE',  ( 1.000000000000000000, 0.000000000000000000, 0.000000000000000000 ) ) ;
#583=DIRECTION ( 'NONE',  ( 0.000000000000000000, 1.000000000000000000, 0.000000000000000000 ) ) ;
#610=EDGE_LOOP ( 'NONE', ( #17972, #13262, #16216, #12238 ) ) ;
#617=CARTESIAN_POINT ( 'NONE',  ( 2.500000000000000000, 4.700000000000000178, 0.5999999999999999778 ) ) ;
#651=VERTEX_POINT ( 'NONE', #2782 ) ;
#676=ADVANCED_FACE ( 'NONE', ( #14257 ), #8520, .T. ) ;
#678=LINE ( 'NONE', #7808, #7149 ) ;
#680=ORIENTED_EDGE ( 'NONE', *, *, #8608, .T. ) ;
#700=ORIENTED_EDGE ( 'NONE', *, *, #7126, .T. ) ;
#704=DIRECTION ( 'NONE',  ( 0.000000000000000000, -1.000000000000000000, 0.000000000000000000 ) ) ;
#726=ORIENTED_EDGE ( 'NONE', *, *, #13, .T. ) ;
#734=DIRECTION ( 'NONE',  ( 1.000000000000000000, 0.000000000000000000, 0.000000000000000000 ) ) ;
#742=LINE ( 'NONE', #15203, #4415 ) ;
#744=PLANE ( 'NONE',  #2004 ) ;
#749=CARTESIAN_POINT ( 'NONE',  ( 1.899999999999999911, 11.40000000000000036, 0.5999999999999999778 ) ) ;
#761=EDGE_CURVE ( 'NONE', #3042, #17417, #10351, .T. ) ;
#791=FACE_OUTER_BOUND ( 'NONE', #7316, .T. ) ;
#795=EDGE_LOOP ( 'NONE', ( #2285, #12347, #15673, #9124 ) ) ;
#809=VECTOR ( 'NONE', #12432, 1000.000000000000000 ) ;
#819=AXIS2_PLACEMENT_3D ( 'NONE', #1636, #253, #11619 ) ;
#837=CARTESIAN_POINT ( 'NONE',  ( -1.899999999999999911, 7.299999999999999822, 1.600000000000000089 ) ) ;
#844=DIRECTION ( 'NONE',  ( 3.172065784643300034E-16, -1.000000000000000000, -1.586032892321649771E-16 ) ) ;
#862=DIRECTION ( 'NONE',  ( 1.708035422500239940E-16, -1.000000000000000000, -4.270088556250599234E-17 ) ) ;
#869=ORIENTED_EDGE ( 'NONE', *, *, #1000, .F. ) ;
#891=DIRECTION ( 'NONE',  ( -3.172065784643300034E-16, 1.000000000000000000, 0.000000000000000000 ) ) ;
#896=PLANE ( 'NONE',  #3171 ) ;
#903=PLANE ( 'NONE',  #13840 ) ;
#938=DIRECTION ( 'NONE',  ( -1.734723475976809806E-16, 1.000000000000000000, 6.938893903907229610E-17 ) ) ;
#945=ORIENTED_EDGE ( 'NONE', *, *, #2348, .T. ) ;
#946=DIRECTION ( 'NONE',  ( 2.220446049250309876E-16, 1.110223024625159992E-16, -1.000000000000000000 ) ) ;
#962=PLANE ( 'NONE',  #17086 ) ;
#979=PLANE ( 'NONE',  #13237 ) ;
#985=DIRECTION ( 'NONE',  ( 1.000000000000000000, 1.908195823574489776E-16, 1.110223024625159992E-16 ) ) ;
#1000=EDGE_CURVE ( 'NONE', #11463, #8080, #17800, .T. ) ;
#1001=DIRECTION ( 'NONE',  ( -1.708035422500239940E-16, 1.000000000000000000, 0.000000000000000000 ) ) ;
#1013=ORIENTED_EDGE ( 'NONE', *, *, #1671, .F. ) ;
#1031=CARTESIAN_POINT ( 'NONE',  ( -2.500000000000000000, 7.299999999999999822, 1.600000000000000089 ) ) ;
#1035=STYLED_ITEM ( 'NONE', ( #2676 ), #2155 ) ;
#1037=ORIENTED_EDGE ( 'NONE', *, *, #9794, .T. ) ;
#1059=VERTEX_POINT ( 'NONE', #14024 ) ;
#1068=ORIENTED_EDGE ( 'NONE', *, *, #5750, .F. ) ;
#1072=APPLICATION_CONTEXT ( 'automotive_design' ) ;
#1090=LINE ( 'NONE', #16648, #279 ) ;
#1092=VECTOR ( 'NONE', #4555, 1000.000000000000000 ) ;
#1127=PLANE ( 'NONE',  #6263 ) ;
#1136=VECTOR ( 'NONE', #10624, 1000.000000000000000 ) ;
#1139=VECTOR ( 'NONE', #16114, 1000.000000000000000 ) ;
#1219=EDGE_LOOP ( 'NONE', ( #14780, #16677, #16057, #10611 ) ) ;
#1239=ORIENTED_EDGE ( 'NONE', *, *, #17143, .T. ) ;
#1243=( LENGTH_UNIT ( ) NAMED_UNIT ( * ) SI_UNIT ( .MILLI., .METRE. ) );
#1300=VERTEX_POINT ( 'NONE', #7364 ) ;
#1308=LINE ( 'NONE', #8629, #11152 ) ;
#1309=LINE ( 'NONE', #8358, #17308 ) ;
#1316=EDGE_LOOP ( 'NONE', ( #3594, #10951, #16968, #14515 ) ) ;
#1321=CARTESIAN_POINT ( 'NONE',  ( 0.1749999999999999889, 2.700000000000000178, 0.5999999999999999778 ) ) ;
#1342=VECTOR ( 'NONE', #8161, 1000.000000000000000 ) ;
#1350=DIRECTION ( 'NONE',  ( -0.000000000000000000, 1.000000000000000000, 0.000000000000000000 ) ) ;
#1358=DIRECTION ( 'NONE',  ( 0.000000000000000000, -1.000000000000000000, 0.000000000000000000 ) ) ;
#1374=EDGE_CURVE ( 'NONE', #9933, #5569, #12126, .T. ) ;
#1412=VECTOR ( 'NONE', #15765, 1000.000000000000000 ) ;
#1422=ORIENTED_EDGE ( 'NONE', *, *, #12562, .F. ) ;
#1439=ORIENTED_EDGE ( 'NONE', *, *, #16868, .T. ) ;
#1444=VECTOR ( 'NONE', #13642, 1000.000000000000000 ) ;
#1445=ORIENTED_EDGE ( 'NONE', *, *, #14789, .F. ) ;
#1449=EDGE_CURVE ( 'NONE', #16145, #12528, #13775, .T. ) ;
#1457=CARTESIAN_POINT ( 'NONE',  ( -0.1749999999999999889, 2.700000000000000178, 1.600000000000000089 ) ) ;
#1472=ORIENTED_EDGE ( 'NONE', *, *, #3297, .F. ) ;
#1474=ORIENTED_EDGE ( 'NONE', *, *, #5686, .F. ) ;
#1477=CARTESIAN_POINT ( 'NONE',  ( -1.899999999999999911, 4.700000000000000178, 1.600000000000000089 ) ) ;
#1484=LINE ( 'NONE', #13971, #3607 ) ;
#1486=LINE ( 'NONE', #14059, #12337 ) ;
#1490=PLANE ( 'NONE',  #15912 ) ;
#1494=ORIENTED_EDGE ( 'NONE', *, *, #5910, .F. ) ;
#1532=DIRECTION ( 'NONE',  ( -1.908195823574489776E-16, 1.000000000000000000, 1.387778780781449866E-16 ) ) ;
#1539=DIRECTION ( 'NONE',  ( -1.708035422500239940E-16, 1.000000000000000000, 0.000000000000000000 ) ) ;
#1553=CARTESIAN_POINT ( 'NONE',  ( 2.500000000000000000, 2.799999999999999822, 1.600000000000000089 ) ) ;
#1570=CARTESIAN_POINT ( 'NONE',  ( 0.1749999999999999889, 2.700000000000000178, 1.600000000000000089 ) ) ;
#1588=VERTEX_POINT ( 'NONE', #13026 ) ;
#1590=VERTEX_POINT ( 'NONE', #6167 ) ;
#1595=DIRECTION ( 'NONE',  ( 1.000000000000000000, 0.000000000000000000, 0.000000000000000000 ) ) ;
#1611=ADVANCED_FACE ( 'NONE', ( #7472 ), #10151, .T. ) ;
#1613=PRODUCT_CONTEXT ( 'NONE', #4584, 'mechanical' ) ;
#1626=ORIENTED_EDGE ( 'NONE', *, *, #7917, .T. ) ;
#1636=CARTESIAN_POINT ( 'NONE',  ( -1.899999999999999911, 2.799999999999999822, 1.600000000000000089 ) ) ;
#1671=EDGE_CURVE ( 'NONE', #17897, #14849, #14414, .T. ) ;
#1674=CARTESIAN_POINT ( 'NONE',  ( -1.899999999999999911, 2.000000000000000000, 0.5999999999999999778 ) ) ;
#1685=CARTESIAN_POINT ( 'NONE',  ( 1.899999999999999911, 2.799999999999999822, 1.600000000000000089 ) ) ;
#1719=VECTOR ( 'NONE', #13446, 1000.000000000000000 ) ;
#1725=VECTOR ( 'NONE', #10887, 1000.000000000000000 ) ;
#1726=DIRECTION ( 'NONE',  ( 2.220446049250309876E-16, 0.000000000000000000, -1.000000000000000000 ) ) ;
#1727=VECTOR ( 'NONE', #3209, 1000.000000000000000 ) ;
#1739=DIRECTION ( 'NONE',  ( 1.110223024625159992E-16, 0.000000000000000000, -1.000000000000000000 ) ) ;
#1744=VERTEX_POINT ( 'NONE', #1906 ) ;
#1761=DIRECTION ( 'NONE',  ( 1.000000000000000000, 0.000000000000000000, 4.440892098500630106E-16 ) ) ;
#1765=CARTESIAN_POINT ( 'NONE',  ( 1.899999999999999911, 9.199999999999999289, 0.5999999999999999778 ) ) ;
#1774=PLANE ( 'NONE',  #4022 ) ;
#1789=EDGE_LOOP ( 'NONE', ( #12555, #11012, #7801, #5145 ) ) ;
#1797=EDGE_CURVE ( 'NONE', #17265, #4743, #6333, .T. ) ;
#1833=ORIENTED_EDGE ( 'NONE', *, *, #8135, .F. ) ;
#1839=DIRECTION ( 'NONE',  ( -1.000000000000000000, 0.000000000000000000, 0.000000000000000000 ) ) ;
#1845=CARTESIAN_POINT ( 'NONE',  ( 2.500000000000000000, 10.00000000000000000, 0.5999999999999999778 ) ) ;
#1847=CARTESIAN_POINT ( 'NONE',  ( -1.899999999999999911, 10.00000000000000000, 0.5999999999999999778 ) ) ;
#1878=CARTESIAN_POINT ( 'NONE',  ( -2.500000000000000000, 4.700000000000000178, 1.600000000000000089 ) ) ;
#1883=ADVANCED_FACE ( 'NONE', ( #15296 ), #1127, .F. ) ;
#1888=CARTESIAN_POINT ( 'NONE',  ( -1.899999999999999911, 9.199999999999999289, 1.600000000000000089 ) ) ;
#1906=CARTESIAN_POINT ( 'NONE',  ( 1.899999999999999911, 4.700000000000000178, 1.600000000000000089 ) ) ;
#1914=ORIENTED_EDGE ( 'NONE', *, *, #16282, .F. ) ;
#1925=FACE_OUTER_BOUND ( 'NONE', #6248, .T. ) ;
#1941=LINE ( 'NONE', #566, #1139 ) ;
#1946=VERTEX_POINT ( 'NONE', #15479 ) ;
#1948=LINE ( 'NONE', #749, #16509 ) ;
#1956=CARTESIAN_POINT ( 'NONE',  ( -2.500000000000000000, 2.000000000000000000, 1.600000000000000089 ) ) ;
#1969=AXIS2_PLACEMENT_3D ( 'NONE', #12920, #1350, #15714 ) ;
#2004=AXIS2_PLACEMENT_3D ( 'NONE', #10840, #5097, #7983 ) ;
#2025=CARTESIAN_POINT ( 'NONE',  ( 0.1749999999999999889, 5.200000000000000178, 0.5999999999999999778 ) ) ;
#2035=EDGE_CURVE ( 'NONE', #13116, #5609, #5925, .T. ) ;
#2051=DIRECTION ( 'NONE',  ( -1.000000000000000000, 0.000000000000000000, 0.000000000000000000 ) ) ;
#2054=DIRECTION ( 'NONE',  ( -4.440892098500630106E-16, 0.000000000000000000, 1.000000000000000000 ) ) ;
#2080=LINE ( 'NONE', #15070, #3772 ) ;
#2083=ORIENTED_EDGE ( 'NONE', *, *, #16513, .F. ) ;
#2095=EDGE_LOOP ( 'NONE', ( #12733, #15704, #149, #5080 ) ) ;
#2098=CARTESIAN_POINT ( 'NONE',  ( 0.1749999999999999889, 5.200000000000000178, 1.600000000000000089 ) ) ;
#2125=EDGE_CURVE ( 'NONE', #1744, #6036, #14701, .T. ) ;
#2126=CARTESIAN_POINT ( 'NONE',  ( -0.1749999999999999889, 9.299999999999998934, 1.600000000000000089 ) ) ;
#2130=ADVANCED_FACE ( 'NONE', ( #548 ), #16192, .F. ) ;
#2131=LINE ( 'NONE', #16031, #13550 ) ;
#2155=MANIFOLD_SOLID_BREP ( 'Stock-MAS-687-1', #2859 ) ;
#2156=VECTOR ( 'NONE', #6839, 1000.000000000000000 ) ;
#2180=ORIENTED_EDGE ( 'NONE', *, *, #4754, .T. ) ;
#2184=ORIENTED_EDGE ( 'NONE', *, *, #14180, .F. ) ;
#2193=DIRECTION ( 'NONE',  ( 2.220446049250309876E-16, 0.000000000000000000, -1.000000000000000000 ) ) ;
#2203=DIRECTION ( 'NONE',  ( 1.000000000000000000, 0.000000000000000000, 0.000000000000000000 ) ) ;
#2206=DIRECTION ( 'NONE',  ( -3.172065784643300034E-16, 1.000000000000000000, 1.586032892321649771E-16 ) ) ;
#2231=FACE_OUTER_BOUND ( 'NONE', #2270, .T. ) ;
#2242=DIRECTION ( 'NONE',  ( -1.908195823574489776E-16, 1.000000000000000000, 0.000000000000000000 ) ) ;
#2243=ORIENTED_EDGE ( 'NONE', *, *, #16405, .F. ) ;
#2245=LINE ( 'NONE', #13545, #17944 ) ;
#2248=ORIENTED_EDGE ( 'NONE', *, *, #6179, .T. ) ;
#2249=EDGE_CURVE ( 'NONE', #15397, #14568, #12147, .T. ) ;
#2270=EDGE_LOOP ( 'NONE', ( #2314, #8742, #10463, #4039 ) ) ;
#2285=ORIENTED_EDGE ( 'NONE', *, *, #4500, .T. ) ;
#2287=CARTESIAN_POINT ( 'NONE',  ( -1.899999999999999911, 10.00000000000000000, 1.600000000000000089 ) ) ;
#2288=DIRECTION ( 'NONE',  ( -0.000000000000000000, 1.000000000000000000, 0.000000000000000000 ) ) ;
#2309=VECTOR ( 'NONE', #1839, 1000.000000000000000 ) ;
#2310=CARTESIAN_POINT ( 'NONE',  ( -0.1749999999999999889, 9.299999999999998934, 1.600000000000000089 ) ) ;
#2314=ORIENTED_EDGE ( 'NONE', *, *, #4250, .F. ) ;
#2325=AXIS2_PLACEMENT_3D ( 'NONE', #13581, #9409, #13672 ) ;
#2328=VECTOR ( 'NONE', #2206, 1000.000000000000000 ) ;
#2333=CARTESIAN_POINT ( 'NONE',  ( -1.899999999999999911, 2.799999999999999822, 1.600000000000000089 ) ) ;
#2348=EDGE_CURVE ( 'NONE', #8437, #4854, #10552, .T. ) ;
#2363=EDGE_CURVE ( 'NONE', #13435, #17446, #9548, .T. ) ;
#2376=VERTEX_POINT ( 'NONE', #10661 ) ;
#2393=CARTESIAN_POINT ( 'NONE',  ( -1.899999999999999911, 2.000000000000000000, 1.600000000000000089 ) ) ;
#2404=CARTESIAN_POINT ( 'NONE',  ( 2.500000000000000000, 2.000000000000000000, 0.5999999999999999778 ) ) ;
#2426=PLANE ( 'NONE',  #11432 ) ;
#2442=CARTESIAN_POINT ( 'NONE',  ( -2.500000000000000000, 9.199999999999999289, 1.600000000000000089 ) ) ;
#2466=CARTESIAN_POINT ( 'NONE',  ( 2.500000000000000000, 9.199999999999999289, 1.600000000000000089 ) ) ;
#2497=( LENGTH_UNIT ( ) NAMED_UNIT ( * ) SI_UNIT ( .MILLI., .METRE. ) );
#2522=ORIENTED_EDGE ( 'NONE', *, *, #4732, .F. ) ;
#2557=CARTESIAN_POINT ( 'NONE',  ( -2.500000000000000000, 10.00000000000000000, 1.600000000000000089 ) ) ;
#2563=LINE ( 'NONE', #13764, #6730 ) ;
#2568=VERTEX_POINT ( 'NONE', #9434 ) ;
#2572=LINE ( 'NONE', #4225, #17380 ) ;
#2590=EDGE_CURVE ( 'NONE', #16690, #7957, #6557, .T. ) ;
#2595=DIRECTION ( 'NONE',  ( 0.000000000000000000, 1.000000000000000000, 0.000000000000000000 ) ) ;
#2596=AXIS2_PLACEMENT_3D ( 'NONE', #8427, #9907, #12693 ) ;
#2610=ORIENTED_EDGE ( 'NONE', *, *, #2590, .F. ) ;
#2618=CARTESIAN_POINT ( 'NONE',  ( -0.1749999999999999889, 7.700000000000000178, 0.5999999999999999778 ) ) ;
#2638=VECTOR ( 'NONE', #2679, 1000.000000000000000 ) ;
#2676=PRESENTATION_STYLE_ASSIGNMENT (( #8145 ) ) ;
#2679=DIRECTION ( 'NONE',  ( 2.220446049250309876E-16, 4.440892098500630106E-16, -1.000000000000000000 ) ) ;
#2682=EDGE_CURVE ( 'NONE', #10396, #5167, #4547, .T. ) ;
#2705=EDGE_CURVE ( 'NONE', #1300, #2568, #7707, .T. ) ;
#2713=DIRECTION ( 'NONE',  ( 2.220446049250309876E-16, 0.000000000000000000, -1.000000000000000000 ) ) ;
#2722=PLANE ( 'NONE',  #3827 ) ;
#2723=EDGE_LOOP ( 'NONE', ( #1474, #10302, #4304, #11286 ) ) ;
#2729=ORIENTED_EDGE ( 'NONE', *, *, #3034, .F. ) ;
#2737=CARTESIAN_POINT ( 'NONE',  ( 0.1749999999999999889, 9.299999999999998934, 1.600000000000000089 ) ) ;
#2751=EDGE_CURVE ( 'NONE', #16690, #3782, #5109, .T. ) ;
#2782=CARTESIAN_POINT ( 'NONE',  ( -2.500000000000000000, 2.799999999999999822, 1.600000000000000089 ) ) ;
#2784=DIRECTION ( 'NONE',  ( 0.000000000000000000, 0.000000000000000000, 1.000000000000000000 ) ) ;
#2790=ORIENTED_EDGE ( 'NONE', *, *, #2363, .F. ) ;
#2792=EDGE_LOOP ( 'NONE', ( #11954, #5924, #2083, #11587 ) ) ;
#2810=ORIENTED_EDGE ( 'NONE', *, *, #7560, .F. ) ;
#2815=ORIENTED_EDGE ( 'NONE', *, *, #14060, .F. ) ;
#2822=ADVANCED_FACE ( 'NONE', ( #15031 ), #3181, .T. ) ;
#2859=CLOSED_SHELL ( 'NONE', ( #4991, #6069, #15732, #14932, #10275, #3404, #7342, #3353, #1611, #2822, #6796, #13620, #3188, #6203, #676, #9224, #10470, #17040, #6918, #17168, #3251, #6770, #14239, #10827, #14022, #17123, #17821, #17132, #17434, #6408, #7874, #4040, #15633, #2130, #1883, #7239, #11431, #3663, #10083, #3443, #6111, #4390 ) ) ;
#2865=LINE ( 'NONE', #14165, #17559 ) ;
#2867=FACE_OUTER_BOUND ( 'NONE', #1316, .T. ) ;
#2868=EDGE_CURVE ( 'NONE', #1588, #651, #14841, .T. ) ;
#2940=EDGE_CURVE ( 'NONE', #16382, #12528, #16319, .T. ) ;
#2945=CARTESIAN_POINT ( 'NONE',  ( -1.899999999999999911, 10.00000000000000000, 1.600000000000000089 ) ) ;
#2976=CARTESIAN_POINT ( 'NONE',  ( -9.868649107779171166E-17, -3.700743415417190112E-17, 0.5999999999999999778 ) ) ;
#2979=EDGE_LOOP ( 'NONE', ( #2180, #17980, #7832, #15856 ) ) ;
#3001=EDGE_LOOP ( 'NONE', ( #726, #6898, #8837, #4793 ) ) ;
#3034=EDGE_CURVE ( 'NONE', #10505, #12165, #6785, .T. ) ;
#3037=ORIENTED_EDGE ( 'NONE', *, *, #17487, .F. ) ;
#3042=VERTEX_POINT ( 'NONE', #18051 ) ;
#3059=FACE_OUTER_BOUND ( 'NONE', #610, .T. ) ;
#3068=CARTESIAN_POINT ( 'NONE',  ( -1.899999999999999911, 11.40000000000000036, 1.600000000000000089 ) ) ;
#3069=CARTESIAN_POINT ( 'NONE',  ( -1.899999999999999911, 7.299999999999999822, 1.600000000000000089 ) ) ;
#3073=EDGE_CURVE ( 'NONE', #13656, #6275, #2245, .T. ) ;
#3119=ORIENTED_EDGE ( 'NONE', *, *, #3073, .T. ) ;
#3143=DIRECTION ( 'NONE',  ( 0.000000000000000000, -1.000000000000000000, -4.440892098500630106E-16 ) ) ;
#3155=VECTOR ( 'NONE', #583, 1000.000000000000000 ) ;
#3171=AXIS2_PLACEMENT_3D ( 'NONE', #15075, #985, #5050 ) ;
#3181=PLANE ( 'NONE',  #3799 ) ;
#3185=ORIENTED_EDGE ( 'NONE', *, *, #7481, .F. ) ;
#3188=ADVANCED_FACE ( 'NONE', ( #9921 ), #17034, .T. ) ;
#3191=CARTESIAN_POINT ( 'NONE',  ( -2.500000000000000000, 2.799999999999999822, 0.5999999999999999778 ) ) ;
#3201=VECTOR ( 'NONE', #3586, 1000.000000000000000 ) ;
#3209=DIRECTION ( 'NONE',  ( 1.110223024625159992E-16, 0.000000000000000000, -1.000000000000000000 ) ) ;
#3210=CARTESIAN_POINT ( 'NONE',  ( -1.899999999999999911, 9.199999999999999289, 1.600000000000000089 ) ) ;
#3251=ADVANCED_FACE ( 'NONE', ( #15491 ), #8444, .T. ) ;
#3261=ORIENTED_EDGE ( 'NONE', *, *, #12184, .F. ) ;
#3288=EDGE_LOOP ( 'NONE', ( #16286, #14113, #9305, #1422 ) ) ;
#3290=CARTESIAN_POINT ( 'NONE',  ( -2.500000000000000000, 9.199999999999999289, 0.5999999999999999778 ) ) ;
#3297=EDGE_CURVE ( 'NONE', #13591, #17265, #2131, .T. ) ;
#3303=CARTESIAN_POINT ( 'NONE',  ( 0.1749999999999999889, 5.200000000000000178, 1.600000000000000089 ) ) ;
#3306=ORIENTED_EDGE ( 'NONE', *, *, #14930, .T. ) ;
#3345=FACE_OUTER_BOUND ( 'NONE', #17085, .T. ) ;
#3349=CARTESIAN_POINT ( 'NONE',  ( -0.1749999999999999889, 4.299999999999999822, 1.600000000000000089 ) ) ;
#3351=EDGE_CURVE ( 'NONE', #1059, #4743, #8944, .T. ) ;
#3353=ADVANCED_FACE ( 'NONE', ( #431 ), #14589, .T. ) ;
#3373=MECHANICAL_DESIGN_GEOMETRIC_PRESENTATION_REPRESENTATION('',(#1035),#10472);
#3379=ORIENTED_EDGE ( 'NONE', *, *, #13823, .T. ) ;
#3398=ORIENTED_EDGE ( 'NONE', *, *, #5352, .F. ) ;
#3404=ADVANCED_FACE ( 'NONE', ( #8032 ), #11996, .T. ) ;
#3430=AXIS2_PLACEMENT_3D ( 'NONE', #2557, #2288, #6825 ) ;
#3431=EDGE_CURVE ( 'NONE', #8419, #1946, #4855, .T. ) ;
#3443=ADVANCED_FACE ( 'NONE', ( #791 ), #896, .F. ) ;
#3458=VECTOR ( 'NONE', #14361, 1000.000000000000000 ) ;
#3460=DIRECTION ( 'NONE',  ( -1.000000000000000000, 0.000000000000000000, -2.220446049250309876E-16 ) ) ;
#3472=CARTESIAN_POINT ( 'NONE',  ( 1.899999999999999911, 7.299999999999999822, 1.600000000000000089 ) ) ;
#3473=EDGE_CURVE ( 'NONE', #18021, #3042, #10793, .T. ) ;
#3476=EDGE_LOOP ( 'NONE', ( #3739, #10687, #14876, #9565 ) ) ;
#3482=AXIS2_PLACEMENT_3D ( 'NONE', #8784, #4245, #5741 ) ;
#3483=CARTESIAN_POINT ( 'NONE',  ( -0.1749999999999999889, 4.299999999999999822, 1.600000000000000089 ) ) ;
#3500=EDGE_CURVE ( 'NONE', #15477, #5861, #13382, .T. ) ;
#3515=CARTESIAN_POINT ( 'NONE',  ( -2.500000000000000000, 4.700000000000000178, 1.600000000000000089 ) ) ;
#3520=DIRECTION ( 'NONE',  ( -1.908195823574489776E-16, 1.000000000000000000, 6.938893903907229610E-17 ) ) ;
#3540=CARTESIAN_POINT ( 'NONE',  ( 1.899999999999999911, 0.5999999999999999778, 1.600000000000000089 ) ) ;
#3551=CARTESIAN_POINT ( 'NONE',  ( 0.1749999999999999889, 7.700000000000000178, 1.600000000000000089 ) ) ;
#3584=EDGE_CURVE ( 'NONE', #17897, #16690, #3933, .T. ) ;
#3586=DIRECTION ( 'NONE',  ( 1.110223024625159992E-16, 0.000000000000000000, -1.000000000000000000 ) ) ;
#3594=ORIENTED_EDGE ( 'NONE', *, *, #17578, .T. ) ;
#3607=VECTOR ( 'NONE', #15558, 1000.000000000000000 ) ;
#3618=DIRECTION ( 'NONE',  ( 1.110223024625159992E-16, 0.000000000000000000, -1.000000000000000000 ) ) ;
#3646=PLANE ( 'NONE',  #249 ) ;
#3660=CARTESIAN_POINT ( 'NONE',  ( 2.500000000000000000, 7.299999999999999822, 1.600000000000000089 ) ) ;
#3663=ADVANCED_FACE ( 'NONE', ( #3059 ), #12964, .F. ) ;
#3687=ORIENTED_EDGE ( 'NONE', *, *, #4124, .T. ) ;
#3697=CARTESIAN_POINT ( 'NONE',  ( 2.500000000000000000, 9.199999999999999289, 1.600000000000000089 ) ) ;
#3710=EDGE_LOOP ( 'NONE', ( #8903, #4722, #13648, #13411 ) ) ;
#3739=ORIENTED_EDGE ( 'NONE', *, *, #14920, .T. ) ;
#3741=DIRECTION ( 'NONE',  ( 1.000000000000000000, 0.000000000000000000, 0.000000000000000000 ) ) ;
#3742=PLANE ( 'NONE',  #14732 ) ;
#3763=CARTESIAN_POINT ( 'NONE',  ( 0.1749999999999999889, 4.299999999999999822, 0.5999999999999999778 ) ) ;
#3767=VECTOR ( 'NONE', #14107, 1000.000000000000000 ) ;
#3772=VECTOR ( 'NONE', #3741, 1000.000000000000000 ) ;
#3782=VERTEX_POINT ( 'NONE', #14808 ) ;
#3793=FACE_OUTER_BOUND ( 'NONE', #16966, .T. ) ;
#3799=AXIS2_PLACEMENT_3D ( 'NONE', #8834, #4912, #2054 ) ;
#3827=AXIS2_PLACEMENT_3D ( 'NONE', #16541, #120, #16877 ) ;
#3850=AXIS2_PLACEMENT_3D ( 'NONE', #3303, #15902, #265 ) ;
#3862=CARTESIAN_POINT ( 'NONE',  ( 1.899999999999999911, 11.40000000000000036, 0.5999999999999999778 ) ) ;
#3891=LINE ( 'NONE', #6767, #12961 ) ;
#3933=LINE ( 'NONE', #15440, #5529 ) ;
#3953=DIRECTION ( 'NONE',  ( 0.000000000000000000, 1.000000000000000000, 2.775557561562890365E-16 ) ) ;
#3988=DIRECTION ( 'NONE',  ( -1.000000000000000000, -3.700743415417190112E-16, 0.000000000000000000 ) ) ;
#4001=FACE_OUTER_BOUND ( 'NONE', #7063, .T. ) ;
#4022=AXIS2_PLACEMENT_3D ( 'NONE', #17205, #4527, #14454 ) ;
#4039=ORIENTED_EDGE ( 'NONE', *, *, #1671, .T. ) ;
#4040=ADVANCED_FACE ( 'NONE', ( #5370 ), #13881, .F. ) ;
#4091=EDGE_CURVE ( 'NONE', #17492, #6294, #11121, .T. ) ;
#4124=EDGE_CURVE ( 'NONE', #5861, #3042, #1309, .T. ) ;
#4144=ORIENTED_EDGE ( 'NONE', *, *, #17863, .T. ) ;
#4146=DIRECTION ( 'NONE',  ( 1.000000000000000000, 0.000000000000000000, 0.000000000000000000 ) ) ;
#4147=CARTESIAN_POINT ( 'NONE',  ( 1.899999999999999911, 4.700000000000000178, 1.600000000000000089 ) ) ;
#4151=EDGE_CURVE ( 'NONE', #17998, #12255, #9643, .T. ) ;
#4161=FACE_OUTER_BOUND ( 'NONE', #309, .T. ) ;
#4164=CARTESIAN_POINT ( 'NONE',  ( 1.899999999999999911, 7.299999999999999822, 0.5999999999999999778 ) ) ;
#4174=LINE ( 'NONE', #6868, #16180 ) ;
#4182=ORIENTED_EDGE ( 'NONE', *, *, #7864, .T. ) ;
#4200=LINE ( 'NONE', #9860, #3767 ) ;
#4225=CARTESIAN_POINT ( 'NONE',  ( -0.1749999999999999889, 2.700000000000000178, 1.600000000000000089 ) ) ;
#4234=CARTESIAN_POINT ( 'NONE',  ( -1.899999999999999911, 0.5999999999999999778, 1.600000000000000089 ) ) ;
#4245=DIRECTION ( 'NONE',  ( 1.000000000000000000, 0.000000000000000000, 2.220446049250309876E-16 ) ) ;
#4248=ORIENTED_EDGE ( 'NONE', *, *, #8347, .T. ) ;
#4250=EDGE_CURVE ( 'NONE', #3782, #14849, #5758, .T. ) ;
#4255=EDGE_LOOP ( 'NONE', ( #12305, #7340, #6947, #11853 ) ) ;
#4276=ORIENTED_EDGE ( 'NONE', *, *, #1000, .T. ) ;
#4277=EDGE_CURVE ( 'NONE', #17446, #17990, #6105, .T. ) ;
#4286=ORIENTED_EDGE ( 'NONE', *, *, #5296, .F. ) ;
#4304=ORIENTED_EDGE ( 'NONE', *, *, #11770, .F. ) ;
#4305=DIRECTION ( 'NONE',  ( -1.734723475976809806E-16, 1.000000000000000000, 0.000000000000000000 ) ) ;
#4340=VECTOR ( 'NONE', #14871, 1000.000000000000000 ) ;
#4343=ORIENTED_EDGE ( 'NONE', *, *, #8822, .F. ) ;
#4390=ADVANCED_FACE ( 'NONE', ( #4616, #560, #5934, #10180 ), #1774, .F. ) ;
#4415=VECTOR ( 'NONE', #844, 1000.000000000000000 ) ;
#4418=FACE_OUTER_BOUND ( 'NONE', #6515, .T. ) ;
#4456=LINE ( 'NONE', #1685, #8511 ) ;
#4457=CARTESIAN_POINT ( 'NONE',  ( 1.899999999999999911, 11.40000000000000036, 1.600000000000000089 ) ) ;
#4474=CARTESIAN_POINT ( 'NONE',  ( -0.1749999999999999889, 6.799999999999999822, 1.600000000000000089 ) ) ;
#4479=LINE ( 'NONE', #10135, #15925 ) ;
#4484=ORIENTED_EDGE ( 'NONE', *, *, #8374, .F. ) ;
#4500=EDGE_CURVE ( 'NONE', #14793, #15397, #17660, .T. ) ;
#4527=DIRECTION ( 'NONE',  ( 1.233581138472399909E-16, 6.167905692361979821E-17, -1.000000000000000000 ) ) ;
#4537=EDGE_CURVE ( 'NONE', #11911, #1590, #7867, .T. ) ;
#4547=LINE ( 'NONE', #10386, #15004 ) ;
#4555=DIRECTION ( 'NONE',  ( 2.220446049250309876E-16, 0.000000000000000000, -1.000000000000000000 ) ) ;
#4563=ORIENTED_EDGE ( 'NONE', *, *, #1374, .T. ) ;
#4580=CARTESIAN_POINT ( 'NONE',  ( 1.899999999999999911, 4.700000000000000178, 1.600000000000000089 ) ) ;
#4584=APPLICATION_CONTEXT ( 'automotive_design' ) ;
#4597=VECTOR ( 'NONE', #2713, 1000.000000000000000 ) ;
#4609=ORIENTED_EDGE ( 'NONE', *, *, #4537, .T. ) ;
#4616=FACE_BOUND ( 'NONE', #9216, .T. ) ;
#4634=VECTOR ( 'NONE', #7283, 1000.000000000000000 ) ;
#4650=LINE ( 'NONE', #1878, #1719 ) ;
#4662=CARTESIAN_POINT ( 'NONE',  ( 0.1749999999999999889, 7.700000000000000178, 1.600000000000000089 ) ) ;
#4663=VECTOR ( 'NONE', #18291, 1000.000000000000000 ) ;
#4711=VECTOR ( 'NONE', #15476, 1000.000000000000000 ) ;
#4714=FACE_OUTER_BOUND ( 'NONE', #4950, .T. ) ;
#4722=ORIENTED_EDGE ( 'NONE', *, *, #5750, .T. ) ;
#4732=EDGE_CURVE ( 'NONE', #5832, #10396, #1484, .T. ) ;
#4735=PLANE ( 'NONE',  #228 ) ;
#4743=VERTEX_POINT ( 'NONE', #7 ) ;
#4754=EDGE_CURVE ( 'NONE', #10130, #15477, #2865, .T. ) ;
#4779=DIRECTION ( 'NONE',  ( -0.000000000000000000, 1.000000000000000000, 0.000000000000000000 ) ) ;
#4792=CARTESIAN_POINT ( 'NONE',  ( -1.899999999999999911, 11.40000000000000036, 0.5999999999999999778 ) ) ;
#4793=ORIENTED_EDGE ( 'NONE', *, *, #6329, .F. ) ;
#4834=ORIENTED_EDGE ( 'NONE', *, *, #1797, .T. ) ;
#4851=EDGE_LOOP ( 'NONE', ( #14290, #1439, #7605, #6489 ) ) ;
#4854=VERTEX_POINT ( 'NONE', #17438 ) ;
#4855=LINE ( 'NONE', #17805, #7064 ) ;
#4878=PLANE ( 'NONE',  #5327 ) ;
#4880=ORIENTED_EDGE ( 'NONE', *, *, #7126, .F. ) ;
#4912=DIRECTION ( 'NONE',  ( -1.000000000000000000, 0.000000000000000000, -4.440892098500630106E-16 ) ) ;
#4919=VECTOR ( 'NONE', #9641, 1000.000000000000000 ) ;
#4941=LINE ( 'NONE', #11987, #14112 ) ;
#4945=LINE ( 'NONE', #2466, #1725 ) ;
#4947=VECTOR ( 'NONE', #6209, 1000.000000000000000 ) ;
#4950=EDGE_LOOP ( 'NONE', ( #11583, #11150, #9356, #10286 ) ) ;
#4962=EDGE_LOOP ( 'NONE', ( #16719, #10035, #17917, #17468 ) ) ;
#4964=VECTOR ( 'NONE', #17473, 1000.000000000000000 ) ;
#4987=ORIENTED_EDGE ( 'NONE', *, *, #6392, .F. ) ;
#4991=ADVANCED_FACE ( 'NONE', ( #13660 ), #10782, .T. ) ;
#5007=CARTESIAN_POINT ( 'NONE',  ( 1.899999999999999911, 2.799999999999999822, 1.600000000000000089 ) ) ;
#5015=CARTESIAN_POINT ( 'NONE',  ( -0.1749999999999999889, 5.200000000000000178, 1.600000000000000089 ) ) ;
#5043=VECTOR ( 'NONE', #8866, 1000.000000000000000 ) ;
#5050=DIRECTION ( 'NONE',  ( -1.908195823574489776E-16, 1.000000000000000000, 0.000000000000000000 ) ) ;
#5059=ORIENTED_EDGE ( 'NONE', *, *, #15508, .F. ) ;
#5063=LINE ( 'NONE', #3483, #1136 ) ;
#5080=ORIENTED_EDGE ( 'NONE', *, *, #6179, .F. ) ;
#5097=DIRECTION ( 'NONE',  ( -1.000000000000000000, -1.908195823574489776E-16, -1.110223024625159992E-16 ) ) ;
#5109=LINE ( 'NONE', #13726, #1444 ) ;
#5122=AXIS2_PLACEMENT_3D ( 'NONE', #3210, #15901, #15999 ) ;
#5133=CARTESIAN_POINT ( 'NONE',  ( -1.899999999999999911, 2.799999999999999822, 0.5999999999999999778 ) ) ;
#5137=CARTESIAN_POINT ( 'NONE',  ( 0.1749999999999999889, 6.799999999999999822, 1.600000000000000089 ) ) ;
#5145=ORIENTED_EDGE ( 'NONE', *, *, #7216, .F. ) ;
#5161=CARTESIAN_POINT ( 'NONE',  ( 0.1749999999999999889, 7.700000000000000178, 1.600000000000000089 ) ) ;
#5167=VERTEX_POINT ( 'NONE', #15610 ) ;
#5169=FILL_AREA_STYLE_COLOUR ( '', #13434 ) ;
#5178=CARTESIAN_POINT ( 'NONE',  ( -1.899999999999999911, 4.700000000000000178, 0.5999999999999999778 ) ) ;
#5210=ORIENTED_EDGE ( 'NONE', *, *, #6782, .F. ) ;
#5246=DIRECTION ( 'NONE',  ( 1.000000000000000000, 1.168655815394900078E-16, 2.220446049250309876E-16 ) ) ;
#5250=AXIS2_PLACEMENT_3D ( 'NONE', #361, #4779, #11555 ) ;
#5296=EDGE_CURVE ( 'NONE', #8570, #10292, #4200, .T. ) ;
#5302=VECTOR ( 'NONE', #17915, 1000.000000000000000 ) ;
#5306=LINE ( 'NONE', #13643, #15289 ) ;
#5322=( NAMED_UNIT ( * ) PLANE_ANGLE_UNIT ( ) SI_UNIT ( $, .RADIAN. ) );
#5327=AXIS2_PLACEMENT_3D ( 'NONE', #6007, #1761, #545 ) ;
#5331=DIRECTION ( 'NONE',  ( 3.700743415417190112E-16, -1.000000000000000000, 8.217301096052200103E-32 ) ) ;
#5352=EDGE_CURVE ( 'NONE', #5832, #16609, #4650, .T. ) ;
#5370=FACE_OUTER_BOUND ( 'NONE', #372, .T. ) ;
#5389=ORIENTED_EDGE ( 'NONE', *, *, #14580, .T. ) ;
#5400=EDGE_LOOP ( 'NONE', ( #13901, #14949, #15505, #7838 ) ) ;
#5425=DIRECTION ( 'NONE',  ( 1.000000000000000000, 1.708035422500239940E-16, 2.736911063134409557E-48 ) ) ;
#5461=VECTOR ( 'NONE', #18041, 1000.000000000000000 ) ;
#5471=ORIENTED_EDGE ( 'NONE', *, *, #4500, .F. ) ;
#5485=DIRECTION ( 'NONE',  ( 4.440892098500630106E-16, 0.000000000000000000, -1.000000000000000000 ) ) ;
#5511=VECTOR ( 'NONE', #10066, 1000.000000000000000 ) ;
#5521=EDGE_CURVE ( 'NONE', #6586, #17729, #11039, .T. ) ;
#5525=AXIS2_PLACEMENT_3D ( 'NONE', #6519, #5331, #10879 ) ;
#5529=VECTOR ( 'NONE', #8203, 1000.000000000000000 ) ;
#5532=VECTOR ( 'NONE', #2051, 1000.000000000000000 ) ;
#5559=DIRECTION ( 'NONE',  ( -0.000000000000000000, 1.000000000000000000, 0.000000000000000000 ) ) ;
#5561=FACE_BOUND ( 'NONE', #18066, .T. ) ;
#5569=VERTEX_POINT ( 'NONE', #5853 ) ;
#5598=ORIENTED_EDGE ( 'NONE', *, *, #16735, .T. ) ;
#5605=AXIS2_PLACEMENT_3D ( 'NONE', #11673, #15851, #567 ) ;
#5609=VERTEX_POINT ( 'NONE', #10114 ) ;
#5630=EDGE_CURVE ( 'NONE', #9279, #17265, #302, .T. ) ;
#5686=EDGE_CURVE ( 'NONE', #4743, #14568, #8636, .T. ) ;
#5737=DIRECTION ( 'NONE',  ( -0.000000000000000000, 1.000000000000000000, 0.000000000000000000 ) ) ;
#5741=DIRECTION ( 'NONE',  ( -2.220446049250309876E-16, 0.000000000000000000, 1.000000000000000000 ) ) ;
#5750=EDGE_CURVE ( 'NONE', #13435, #8906, #4456, .T. ) ;
#5752=VECTOR ( 'NONE', #6274, 1000.000000000000000 ) ;
#5758=LINE ( 'NONE', #2618, #8533 ) ;
#5775=ORIENTED_EDGE ( 'NONE', *, *, #14930, .F. ) ;
#5827=AXIS2_PLACEMENT_3D ( 'NONE', #14710, #3143, #9053 ) ;
#5832=VERTEX_POINT ( 'NONE', #3515 ) ;
#5853=CARTESIAN_POINT ( 'NONE',  ( -1.899999999999999911, 0.5999999999999999778, 0.5999999999999999778 ) ) ;
#5857=VERTEX_POINT ( 'NONE', #9344 ) ;
#5861=VERTEX_POINT ( 'NONE', #8979 ) ;
#5865=VECTOR ( 'NONE', #12316, 1000.000000000000000 ) ;
#5866=VECTOR ( 'NONE', #83, 1000.000000000000000 ) ;
#5871=EDGE_CURVE ( 'NONE', #17998, #8948, #13525, .T. ) ;
#5881=VECTOR ( 'NONE', #9533, 1000.000000000000000 ) ;
#5890=VECTOR ( 'NONE', #9313, 1000.000000000000000 ) ;
#5896=ORIENTED_EDGE ( 'NONE', *, *, #4250, .T. ) ;
#5910=EDGE_CURVE ( 'NONE', #16761, #1744, #1941, .T. ) ;
#5924=ORIENTED_EDGE ( 'NONE', *, *, #16405, .T. ) ;
#5925=LINE ( 'NONE', #13141, #5752 ) ;
#5928=DIRECTION ( 'NONE',  ( 4.440892098500630106E-16, 4.440892098500630106E-16, -1.000000000000000000 ) ) ;
#5932=SHAPE_REPRESENTATION ( 'Insulating Base Plate', ( #17681 ), #11500 ) ;
#5934=FACE_BOUND ( 'NONE', #12960, .T. ) ;
#5950=ORIENTED_EDGE ( 'NONE', *, *, #17100, .F. ) ;
#5954=VERTEX_POINT ( 'NONE', #8075 ) ;
#5956=EDGE_CURVE ( 'NONE', #15379, #7912, #3891, .T. ) ;
#5977=PLANE ( 'NONE',  #819 ) ;
#6003=DIRECTION ( 'NONE',  ( 1.908195823574489776E-16, -1.000000000000000000, -1.387778780781449866E-16 ) ) ;
#6007=CARTESIAN_POINT ( 'NONE',  ( 2.500000000000000000, 2.799999999999999822, 1.600000000000000089 ) ) ;
#6036=VERTEX_POINT ( 'NONE', #11106 ) ;
#6044=CARTESIAN_POINT ( 'NONE',  ( 0.1749999999999999889, 4.299999999999999822, 1.600000000000000089 ) ) ;
#6061=CARTESIAN_POINT ( 'NONE',  ( -1.899999999999999911, 4.700000000000000178, 1.600000000000000089 ) ) ;
#6069=ADVANCED_FACE ( 'NONE', ( #11021 ), #8343, .T. ) ;
#6077=LINE ( 'NONE', #617, #17752 ) ;
#6084=PLANE ( 'NONE',  #5250 ) ;
#6105=LINE ( 'NONE', #11769, #16462 ) ;
#6111=ADVANCED_FACE ( 'NONE', ( #5561, #11208, #16852, #4161 ), #1490, .T. ) ;
#6132=VECTOR ( 'NONE', #5485, 1000.000000000000000 ) ;
#6142=AXIS2_PLACEMENT_3D ( 'NONE', #2126, #9249, #734 ) ;
#6163=CARTESIAN_POINT ( 'NONE',  ( -0.1749999999999999889, 4.299999999999999822, 0.5999999999999999778 ) ) ;
#6167=CARTESIAN_POINT ( 'NONE',  ( -1.899999999999999911, 7.299999999999999822, 0.5999999999999999778 ) ) ;
#6172=ORIENTED_EDGE ( 'NONE', *, *, #15821, .T. ) ;
#6179=EDGE_CURVE ( 'NONE', #1946, #5569, #15553, .T. ) ;
#6192=ORIENTED_EDGE ( 'NONE', *, *, #6392, .T. ) ;
#6203=ADVANCED_FACE ( 'NONE', ( #8523 ), #11476, .T. ) ;
#6209=DIRECTION ( 'NONE',  ( 2.220446049250309876E-16, 0.000000000000000000, -1.000000000000000000 ) ) ;
#6232=CARTESIAN_POINT ( 'NONE',  ( -2.500000000000000000, 10.00000000000000000, 0.5999999999999999778 ) ) ;
#6248=EDGE_LOOP ( 'NONE', ( #13273, #15977, #13076, #225 ) ) ;
#6263=AXIS2_PLACEMENT_3D ( 'NONE', #6772, #16674, #16492 ) ;
#6274=DIRECTION ( 'NONE',  ( 1.908195823574489776E-16, -1.000000000000000000, -6.938893903907229610E-17 ) ) ;
#6275=VERTEX_POINT ( 'NONE', #17276 ) ;
#6294=VERTEX_POINT ( 'NONE', #1847 ) ;
#6328=FACE_OUTER_BOUND ( 'NONE', #2095, .T. ) ;
#6329=EDGE_CURVE ( 'NONE', #12197, #16406, #13008, .T. ) ;
#6333=LINE ( 'NONE', #1321, #8681 ) ;
#6338=CARTESIAN_POINT ( 'NONE',  ( -1.899999999999999911, 4.700000000000000178, 1.600000000000000089 ) ) ;
#6341=ORIENTED_EDGE ( 'NONE', *, *, #5630, .T. ) ;
#6354=LINE ( 'NONE', #12019, #2328 ) ;
#6392=EDGE_CURVE ( 'NONE', #16382, #6586, #11607, .T. ) ;
#6408=ADVANCED_FACE ( 'NONE', ( #2231 ), #744, .F. ) ;
#6460=VECTOR ( 'NONE', #7583, 1000.000000000000000 ) ;
#6466=ORIENTED_EDGE ( 'NONE', *, *, #13199, .F. ) ;
#6474=ORIENTED_EDGE ( 'NONE', *, *, #6563, .T. ) ;
#6478=VECTOR ( 'NONE', #1001, 1000.000000000000000 ) ;
#6479=DIRECTION ( 'NONE',  ( 2.220446049250309876E-16, 0.000000000000000000, -1.000000000000000000 ) ) ;
#6489=ORIENTED_EDGE ( 'NONE', *, *, #18289, .F. ) ;
#6495=EDGE_CURVE ( 'NONE', #15295, #13116, #9895, .T. ) ;
#6515=EDGE_LOOP ( 'NONE', ( #12253, #13717, #12617, #14585 ) ) ;
#6519=CARTESIAN_POINT ( 'NONE',  ( -1.899999999999999911, 2.000000000000000000, 1.600000000000000089 ) ) ;
#6521=DIRECTION ( 'NONE',  ( -1.000000000000000000, -3.700743415417190112E-16, -3.700743415417190112E-16 ) ) ;
#6525=EDGE_LOOP ( 'NONE', ( #15621, #5598, #13381, #9679 ) ) ;
#6527=EDGE_CURVE ( 'NONE', #1744, #13435, #7210, .T. ) ;
#6529=DIRECTION ( 'NONE',  ( 1.000000000000000000, 3.172065784643300034E-16, 2.220446049250309876E-16 ) ) ;
#6540=EDGE_CURVE ( 'NONE', #12255, #5832, #14156, .T. ) ;
#6541=CARTESIAN_POINT ( 'NONE',  ( 2.500000000000000000, 2.799999999999999822, 1.600000000000000089 ) ) ;
#6557=LINE ( 'NONE', #2310, #10547 ) ;
#6563=EDGE_CURVE ( 'NONE', #7957, #7912, #9806, .T. ) ;
#6586=VERTEX_POINT ( 'NONE', #14054 ) ;
#6600=DIRECTION ( 'NONE',  ( 1.000000000000000000, 0.000000000000000000, 0.000000000000000000 ) ) ;
#6611=DIRECTION ( 'NONE',  ( -1.168655815394900078E-16, 1.000000000000000000, 5.843279076974510248E-17 ) ) ;
#6720=AXIS2_PLACEMENT_3D ( 'NONE', #4580, #5246, #17728 ) ;
#6728=VECTOR ( 'NONE', #11344, 1000.000000000000000 ) ;
#6730=VECTOR ( 'NONE', #6733, 1000.000000000000000 ) ;
#6733=DIRECTION ( 'NONE',  ( 0.000000000000000000, -1.000000000000000000, -1.387778780781449866E-16 ) ) ;
#6745=CARTESIAN_POINT ( 'NONE',  ( -1.899999999999999911, 9.199999999999999289, 0.5999999999999999778 ) ) ;
#6767=CARTESIAN_POINT ( 'NONE',  ( 0.1749999999999999889, 9.299999999999998934, 0.5999999999999999778 ) ) ;
#6770=ADVANCED_FACE ( 'NONE', ( #14879 ), #7395, .T. ) ;
#6772=CARTESIAN_POINT ( 'NONE',  ( 0.1749999999999999889, 2.700000000000000178, 1.600000000000000089 ) ) ;
#6782=EDGE_CURVE ( 'NONE', #16101, #9670, #13759, .T. ) ;
#6785=LINE ( 'NONE', #7893, #809 ) ;
#6795=DIRECTION ( 'NONE',  ( 0.000000000000000000, 1.110223024625159992E-16, -1.000000000000000000 ) ) ;
#6796=ADVANCED_FACE ( 'NONE', ( #12381 ), #14977, .T. ) ;
#6825=DIRECTION ( 'NONE',  ( 1.000000000000000000, 0.000000000000000000, 0.000000000000000000 ) ) ;
#6839=DIRECTION ( 'NONE',  ( -1.000000000000000000, 0.000000000000000000, -3.700743415417190112E-16 ) ) ;
#6842=VERTEX_POINT ( 'NONE', #3660 ) ;
#6860=ORIENTED_EDGE ( 'NONE', *, *, #5956, .T. ) ;
#6868=CARTESIAN_POINT ( 'NONE',  ( -1.899999999999999911, 2.000000000000000000, 1.600000000000000089 ) ) ;
#6898=ORIENTED_EDGE ( 'NONE', *, *, #8575, .T. ) ;
#6910=FACE_OUTER_BOUND ( 'NONE', #15910, .T. ) ;
#6918=ADVANCED_FACE ( 'NONE', ( #6910 ), #8483, .T. ) ;
#6919=ORIENTED_EDGE ( 'NONE', *, *, #15261, .F. ) ;
#6947=ORIENTED_EDGE ( 'NONE', *, *, #13946, .F. ) ;
#6963=ORIENTED_EDGE ( 'NONE', *, *, #13850, .T. ) ;
#6980=ORIENTED_EDGE ( 'NONE', *, *, #15750, .T. ) ;
#7043=CARTESIAN_POINT ( 'NONE',  ( -2.500000000000000000, 2.799999999999999822, 0.5999999999999999778 ) ) ;
#7052=VECTOR ( 'NONE', #10399, 1000.000000000000000 ) ;
#7063=EDGE_LOOP ( 'NONE', ( #14631, #2248, #7185, #12534 ) ) ;
#7064=VECTOR ( 'NONE', #12189, 1000.000000000000000 ) ;
#7075=VECTOR ( 'NONE', #6600, 1000.000000000000000 ) ;
#7082=EDGE_LOOP ( 'NONE', ( #7194, #11633, #4834, #12841 ) ) ;
#7126=EDGE_CURVE ( 'NONE', #12165, #10292, #12657, .T. ) ;
#7133=ORIENTED_EDGE ( 'NONE', *, *, #6563, .F. ) ;
#7140=DIRECTION ( 'NONE',  ( 0.000000000000000000, -1.000000000000000000, 0.000000000000000000 ) ) ;
#7145=DIRECTION ( 'NONE',  ( 1.000000000000000000, 0.000000000000000000, 0.000000000000000000 ) ) ;
#7149=VECTOR ( 'NONE', #16236, 1000.000000000000000 ) ;
#7160=DIRECTION ( 'NONE',  ( 1.000000000000000000, 0.000000000000000000, 1.850371707708589879E-16 ) ) ;
#7168=CARTESIAN_POINT ( 'NONE',  ( 0.1749999999999999889, 4.299999999999999822, 0.5999999999999999778 ) ) ;
#7185=ORIENTED_EDGE ( 'NONE', *, *, #1374, .F. ) ;
#7189=LINE ( 'NONE', #10133, #12433 ) ;
#7194=ORIENTED_EDGE ( 'NONE', *, *, #8374, .T. ) ;
#7197=LINE ( 'NONE', #8753, #5511 ) ;
#7210=LINE ( 'NONE', #4147, #4663 ) ;
#7211=ORIENTED_EDGE ( 'NONE', *, *, #8312, .T. ) ;
#7216=EDGE_CURVE ( 'NONE', #16761, #6275, #15449, .T. ) ;
#7225=ORIENTED_EDGE ( 'NONE', *, *, #12132, .T. ) ;
#7239=ADVANCED_FACE ( 'NONE', ( #8485 ), #10139, .F. ) ;
#7282=VECTOR ( 'NONE', #13044, 1000.000000000000000 ) ;
#7283=DIRECTION ( 'NONE',  ( 2.220446049250309876E-16, 0.000000000000000000, -1.000000000000000000 ) ) ;
#7300=CARTESIAN_POINT ( 'NONE',  ( -0.1749999999999999889, 9.299999999999998934, 0.5999999999999999778 ) ) ;
#7316=EDGE_LOOP ( 'NONE', ( #476, #8406, #869, #6963 ) ) ;
#7337=DIRECTION ( 'NONE',  ( 2.220446049250309876E-16, 0.000000000000000000, -1.000000000000000000 ) ) ;
#7340=ORIENTED_EDGE ( 'NONE', *, *, #4091, .T. ) ;
#7342=ADVANCED_FACE ( 'NONE', ( #3345 ), #4735, .T. ) ;
#7364=CARTESIAN_POINT ( 'NONE',  ( 2.500000000000000000, 2.000000000000000000, 1.600000000000000089 ) ) ;
#7376=ORIENTED_EDGE ( 'NONE', *, *, #10570, .T. ) ;
#7383=PRODUCT_DEFINITION_FORMATION_WITH_SPECIFIED_SOURCE ( 'ANY', '', #7704, .NOT_KNOWN. ) ;
#7395=PLANE ( 'NONE',  #6720 ) ;
#7421=DIRECTION ( 'NONE',  ( 4.440892098500630106E-16, 0.000000000000000000, -1.000000000000000000 ) ) ;
#7458=LINE ( 'NONE', #4662, #14715 ) ;
#7459=LINE ( 'NONE', #1888, #13926 ) ;
#7472=FACE_OUTER_BOUND ( 'NONE', #3288, .T. ) ;
#7481=EDGE_CURVE ( 'NONE', #5167, #1590, #12429, .T. ) ;
#7493=VECTOR ( 'NONE', #1739, 1000.000000000000000 ) ;
#7494=CARTESIAN_POINT ( 'NONE',  ( 0.1749999999999999889, 4.299999999999999822, 1.600000000000000089 ) ) ;
#7495=EDGE_LOOP ( 'NONE', ( #3037, #16211, #14151, #13802 ) ) ;
#7560=EDGE_CURVE ( 'NONE', #16101, #1588, #4174, .T. ) ;
#7583=DIRECTION ( 'NONE',  ( 1.000000000000000000, 0.000000000000000000, 0.000000000000000000 ) ) ;
#7605=ORIENTED_EDGE ( 'NONE', *, *, #10395, .F. ) ;
#7610=CARTESIAN_POINT ( 'NONE',  ( -2.500000000000000000, 7.299999999999999822, 1.600000000000000089 ) ) ;
#7626=VECTOR ( 'NONE', #9337, 1000.000000000000000 ) ;
#7647=CARTESIAN_POINT ( 'NONE',  ( -1.899999999999999911, 7.299999999999999822, 1.600000000000000089 ) ) ;
#7684=PLANE ( 'NONE',  #5827 ) ;
#7704=PRODUCT ( 'Insulating Base Plate', 'Insulating Base Plate', '', ( #1613 ) ) ;
#7707=LINE ( 'NONE', #14737, #5532 ) ;
#7745=ADVANCED_BREP_SHAPE_REPRESENTATION ( '', ( #2155, #17681 ), #11500 ) ;
#7746=ORIENTED_EDGE ( 'NONE', *, *, #9159, .F. ) ;
#7801=ORIENTED_EDGE ( 'NONE', *, *, #12132, .F. ) ;
#7808=CARTESIAN_POINT ( 'NONE',  ( 1.899999999999999911, 2.000000000000000000, 1.600000000000000089 ) ) ;
#7813=VECTOR ( 'NONE', #3520, 1000.000000000000000 ) ;
#7825=CARTESIAN_POINT ( 'NONE',  ( -1.899999999999999911, 10.00000000000000000, 1.600000000000000089 ) ) ;
#7832=ORIENTED_EDGE ( 'NONE', *, *, #18074, .F. ) ;
#7834=EDGE_LOOP ( 'NONE', ( #16130, #9851, #2184, #10333 ) ) ;
#7836=FACE_OUTER_BOUND ( 'NONE', #17951, .T. ) ;
#7838=ORIENTED_EDGE ( 'NONE', *, *, #16735, .F. ) ;
#7864=EDGE_CURVE ( 'NONE', #5954, #16609, #16579, .T. ) ;
#7867=LINE ( 'NONE', #837, #12312 ) ;
#7868=AXIS2_PLACEMENT_3D ( 'NONE', #8274, #10674, #2242 ) ;
#7874=ADVANCED_FACE ( 'NONE', ( #13419 ), #11940, .F. ) ;
#7893=CARTESIAN_POINT ( 'NONE',  ( 1.899999999999999911, 9.199999999999999289, 1.600000000000000089 ) ) ;
#7912=VERTEX_POINT ( 'NONE', #10738 ) ;
#7917=EDGE_CURVE ( 'NONE', #6842, #16761, #16385, .T. ) ;
#7957=VERTEX_POINT ( 'NONE', #8336 ) ;
#7966=FILL_AREA_STYLE ('',( #5169 ) ) ;
#7983=DIRECTION ( 'NONE',  ( -1.908195823574489776E-16, 1.000000000000000000, 0.000000000000000000 ) ) ;
#8012=ORIENTED_EDGE ( 'NONE', *, *, #3431, .F. ) ;
#8022=CARTESIAN_POINT ( 'NONE',  ( -2.500000000000000000, 4.700000000000000178, 0.5999999999999999778 ) ) ;
#8028=DIRECTION ( 'NONE',  ( -3.172065784643300034E-16, 1.000000000000000000, 0.000000000000000000 ) ) ;
#8031=ORIENTED_EDGE ( 'NONE', *, *, #2940, .F. ) ;
#8032=FACE_OUTER_BOUND ( 'NONE', #17099, .T. ) ;
#8051=FACE_OUTER_BOUND ( 'NONE', #6525, .T. ) ;
#8075=CARTESIAN_POINT ( 'NONE',  ( -1.899999999999999911, 4.700000000000000178, 0.5999999999999999778 ) ) ;
#8080=VERTEX_POINT ( 'NONE', #17267 ) ;
#8084=ORIENTED_EDGE ( 'NONE', *, *, #18074, .T. ) ;
#8097=CARTESIAN_POINT ( 'NONE',  ( 1.899999999999999911, 0.5999999999999999778, 1.600000000000000089 ) ) ;
#8135=EDGE_CURVE ( 'NONE', #14793, #13591, #5063, .T. ) ;
#8136=LINE ( 'NONE', #5161, #3201 ) ;
#8140=DIRECTION ( 'NONE',  ( -1.000000000000000000, -1.168655815394900078E-16, -1.168655815394900078E-16 ) ) ;
#8145=SURFACE_STYLE_USAGE ( .BOTH. , #10819 ) ;
#8147=CARTESIAN_POINT ( 'NONE',  ( -1.899999999999999911, 9.199999999999999289, 1.600000000000000089 ) ) ;
#8161=DIRECTION ( 'NONE',  ( 1.000000000000000000, 0.000000000000000000, 0.000000000000000000 ) ) ;
#8175=ORIENTED_EDGE ( 'NONE', *, *, #9693, .T. ) ;
#8199=CARTESIAN_POINT ( 'NONE',  ( -0.1749999999999999889, 2.700000000000000178, 0.5999999999999999778 ) ) ;
#8200=VECTOR ( 'NONE', #16439, 1000.000000000000000 ) ;
#8203=DIRECTION ( 'NONE',  ( -1.908195823574489776E-16, 1.000000000000000000, 1.387778780781449866E-16 ) ) ;
#8234=CARTESIAN_POINT ( 'NONE',  ( 1.899999999999999911, 2.799999999999999822, 0.5999999999999999778 ) ) ;
#8236=VECTOR ( 'NONE', #15464, 1000.000000000000000 ) ;
#8262=PRODUCT_DEFINITION_CONTEXT ( 'detailed design', #1072, 'design' ) ;
#8265=AXIS2_PLACEMENT_3D ( 'NONE', #17635, #2203, #14989 ) ;
#8274=CARTESIAN_POINT ( 'NONE',  ( 0.1749999999999999889, 9.299999999999998934, 1.600000000000000089 ) ) ;
#8283=LINE ( 'NONE', #14008, #260 ) ;
#8312=EDGE_CURVE ( 'NONE', #6036, #8906, #14393, .T. ) ;
#8316=DIRECTION ( 'NONE',  ( 1.000000000000000000, 0.000000000000000000, 1.850371707708589879E-16 ) ) ;
#8336=CARTESIAN_POINT ( 'NONE',  ( 0.1749999999999999889, 9.299999999999998934, 1.600000000000000089 ) ) ;
#8343=PLANE ( 'NONE',  #17368 ) ;
#8347=EDGE_CURVE ( 'NONE', #16569, #17897, #7458, .T. ) ;
#8358=CARTESIAN_POINT ( 'NONE',  ( 1.899999999999999911, 10.00000000000000000, 0.5999999999999999778 ) ) ;
#8374=EDGE_CURVE ( 'NONE', #14568, #13591, #4479, .T. ) ;
#8397=CARTESIAN_POINT ( 'NONE',  ( -2.500000000000000000, 2.799999999999999822, 1.600000000000000089 ) ) ;
#8400=DIRECTION ( 'NONE',  ( 0.000000000000000000, 0.000000000000000000, -1.000000000000000000 ) ) ;
#8406=ORIENTED_EDGE ( 'NONE', *, *, #12820, .F. ) ;
#8419=VERTEX_POINT ( 'NONE', #3540 ) ;
#8422=CARTESIAN_POINT ( 'NONE',  ( -2.500000000000000000, 2.799999999999999822, 1.600000000000000089 ) ) ;
#8427=CARTESIAN_POINT ( 'NONE',  ( 1.899999999999999911, 9.199999999999999289, 1.600000000000000089 ) ) ;
#8429=ORIENTED_EDGE ( 'NONE', *, *, #1449, .T. ) ;
#8437=VERTEX_POINT ( 'NONE', #15838 ) ;
#8444=PLANE ( 'NONE',  #11181 ) ;
#8456=VERTEX_POINT ( 'NONE', #17026 ) ;
#8461=EDGE_CURVE ( 'NONE', #1300, #9201, #10012, .T. ) ;
#8483=PLANE ( 'NONE',  #1969 ) ;
#8485=FACE_OUTER_BOUND ( 'NONE', #13050, .T. ) ;
#8511=VECTOR ( 'NONE', #7337, 1000.000000000000000 ) ;
#8520=PLANE ( 'NONE',  #15568 ) ;
#8523=FACE_OUTER_BOUND ( 'NONE', #2979, .T. ) ;
#8532=DIRECTION ( 'NONE',  ( 2.220446049250309876E-16, 0.000000000000000000, -1.000000000000000000 ) ) ;
#8533=VECTOR ( 'NONE', #13912, 1000.000000000000000 ) ;
#8570=VERTEX_POINT ( 'NONE', #1765 ) ;
#8575=EDGE_CURVE ( 'NONE', #10130, #14528, #11306, .T. ) ;
#8585=DIRECTION ( 'NONE',  ( 0.000000000000000000, 1.000000000000000000, 0.000000000000000000 ) ) ;
#8608=EDGE_CURVE ( 'NONE', #16406, #14528, #8883, .T. ) ;
#8629=CARTESIAN_POINT ( 'NONE',  ( -2.500000000000000000, 10.00000000000000000, 0.5999999999999999778 ) ) ;
#8631=DIRECTION ( 'NONE',  ( 0.000000000000000000, 0.000000000000000000, -1.000000000000000000 ) ) ;
#8636=LINE ( 'NONE', #7168, #3458 ) ;
#8681=VECTOR ( 'NONE', #12527, 1000.000000000000000 ) ;
#8723=ORIENTED_EDGE ( 'NONE', *, *, #6527, .F. ) ;
#8732=EDGE_LOOP ( 'NONE', ( #6192, #10496, #1445, #8031 ) ) ;
#8734=LINE ( 'NONE', #16975, #12913 ) ;
#8742=ORIENTED_EDGE ( 'NONE', *, *, #2751, .F. ) ;
#8753=CARTESIAN_POINT ( 'NONE',  ( -1.899999999999999911, 7.299999999999999822, 0.5999999999999999778 ) ) ;
#8784=CARTESIAN_POINT ( 'NONE',  ( 1.899999999999999911, 11.40000000000000036, 1.600000000000000089 ) ) ;
#8800=VECTOR ( 'NONE', #15872, 1000.000000000000000 ) ;
#8805=DIRECTION ( 'NONE',  ( -2.337311630789800155E-16, 1.000000000000000000, 1.168655815394900078E-16 ) ) ;
#8815=VECTOR ( 'NONE', #64, 1000.000000000000000 ) ;
#8822=EDGE_CURVE ( 'NONE', #9265, #16382, #11011, .T. ) ;
#8834=CARTESIAN_POINT ( 'NONE',  ( -2.500000000000000000, 9.199999999999999289, 1.600000000000000089 ) ) ;
#8837=ORIENTED_EDGE ( 'NONE', *, *, #8608, .F. ) ;
#8845=DIRECTION ( 'NONE',  ( -1.000000000000000000, 0.000000000000000000, 0.000000000000000000 ) ) ;
#8852=FACE_OUTER_BOUND ( 'NONE', #2792, .T. ) ;
#8866=DIRECTION ( 'NONE',  ( 1.000000000000000000, 0.000000000000000000, 0.000000000000000000 ) ) ;
#8871=LINE ( 'NONE', #7300, #2309 ) ;
#8878=ORIENTED_EDGE ( 'NONE', *, *, #15501, .T. ) ;
#8879=DIRECTION ( 'NONE',  ( 2.220446049250309876E-16, 0.000000000000000000, -1.000000000000000000 ) ) ;
#8883=LINE ( 'NONE', #4792, #4964 ) ;
#8903=ORIENTED_EDGE ( 'NONE', *, *, #6527, .T. ) ;
#8906=VERTEX_POINT ( 'NONE', #8234 ) ;
#8931=ORIENTED_EDGE ( 'NONE', *, *, #761, .T. ) ;
#8944=LINE ( 'NONE', #10230, #1727 ) ;
#8948=VERTEX_POINT ( 'NONE', #17320 ) ;
#8979=CARTESIAN_POINT ( 'NONE',  ( 1.899999999999999911, 10.00000000000000000, 0.5999999999999999778 ) ) ;
#9001=DIRECTION ( 'NONE',  ( 2.220446049250309876E-16, 0.000000000000000000, -1.000000000000000000 ) ) ;
#9023=ORIENTED_EDGE ( 'NONE', *, *, #2682, .F. ) ;
#9053=DIRECTION ( 'NONE',  ( 0.000000000000000000, 4.440892098500630106E-16, -1.000000000000000000 ) ) ;
#9057=VECTOR ( 'NONE', #11221, 1000.000000000000000 ) ;
#9062=PLANE ( 'NONE',  #5605 ) ;
#9109=DIRECTION ( 'NONE',  ( -2.220446049250309876E-16, 0.000000000000000000, 1.000000000000000000 ) ) ;
#9120=LINE ( 'NONE', #10157, #5043 ) ;
#9121=LINE ( 'NONE', #10614, #10878 ) ;
#9124=ORIENTED_EDGE ( 'NONE', *, *, #13267, .T. ) ;
#9159=EDGE_CURVE ( 'NONE', #11911, #9265, #10110, .T. ) ;
#9166=CARTESIAN_POINT ( 'NONE',  ( 0.1749999999999999889, 6.799999999999999822, 0.5999999999999999778 ) ) ;
#9201=VERTEX_POINT ( 'NONE', #2404 ) ;
#9206=CARTESIAN_POINT ( 'NONE',  ( 1.899999999999999911, 10.00000000000000000, 1.600000000000000089 ) ) ;
#9214=CARTESIAN_POINT ( 'NONE',  ( 2.500000000000000000, 9.199999999999999289, 0.5999999999999999778 ) ) ;
#9216=EDGE_LOOP ( 'NONE', ( #1037, #8878, #3379, #4276 ) ) ;
#9224=ADVANCED_FACE ( 'NONE', ( #8051 ), #18010, .T. ) ;
#9227=LINE ( 'NONE', #12295, #5302 ) ;
#9242=EDGE_CURVE ( 'NONE', #10396, #11911, #9227, .T. ) ;
#9243=ORIENTED_EDGE ( 'NONE', *, *, #2868, .F. ) ;
#9249=DIRECTION ( 'NONE',  ( -0.000000000000000000, 1.000000000000000000, 0.000000000000000000 ) ) ;
#9255=EDGE_CURVE ( 'NONE', #16609, #5167, #14890, .T. ) ;
#9265=VERTEX_POINT ( 'NONE', #10719 ) ;
#9273=ORIENTED_EDGE ( 'NONE', *, *, #7864, .F. ) ;
#9279=VERTEX_POINT ( 'NONE', #9319 ) ;
#9292=LINE ( 'NONE', #5133, #9684 ) ;
#9297=CARTESIAN_POINT ( 'NONE',  ( -1.899999999999999911, 0.5999999999999999778, 1.600000000000000089 ) ) ;
#9305=ORIENTED_EDGE ( 'NONE', *, *, #1449, .F. ) ;
#9313=DIRECTION ( 'NONE',  ( -1.000000000000000000, 0.000000000000000000, 0.000000000000000000 ) ) ;
#9319=CARTESIAN_POINT ( 'NONE',  ( -0.1749999999999999889, 2.700000000000000178, 1.600000000000000089 ) ) ;
#9329=( NAMED_UNIT ( * ) PLANE_ANGLE_UNIT ( ) SI_UNIT ( $, .RADIAN. ) );
#9337=DIRECTION ( 'NONE',  ( 1.708035422500239940E-16, -1.000000000000000000, -8.540177112501209562E-17 ) ) ;
#9344=CARTESIAN_POINT ( 'NONE',  ( -0.1749999999999999889, 5.200000000000000178, 1.600000000000000089 ) ) ;
#9348=CARTESIAN_POINT ( 'NONE',  ( -2.500000000000000000, 9.199999999999999289, 1.600000000000000089 ) ) ;
#9354=EDGE_CURVE ( 'NONE', #8456, #11761, #1090, .T. ) ;
#9356=ORIENTED_EDGE ( 'NONE', *, *, #11513, .F. ) ;
#9402=PLANE ( 'NONE',  #17657 ) ;
#9409=DIRECTION ( 'NONE',  ( -1.000000000000000000, -1.708035422500239940E-16, -4.440892098500630106E-16 ) ) ;
#9410=DIRECTION ( 'NONE',  ( -1.000000000000000000, 0.000000000000000000, 0.000000000000000000 ) ) ;
#9418=ORIENTED_EDGE ( 'NONE', *, *, #16295, .T. ) ;
#9434=CARTESIAN_POINT ( 'NONE',  ( 1.899999999999999911, 2.000000000000000000, 1.600000000000000089 ) ) ;
#9440=ORIENTED_EDGE ( 'NONE', *, *, #17487, .T. ) ;
#9456=FACE_OUTER_BOUND ( 'NONE', #5400, .T. ) ;
#9460=ORIENTED_EDGE ( 'NONE', *, *, #14789, .T. ) ;
#9530=ORIENTED_EDGE ( 'NONE', *, *, #4277, .T. ) ;
#9533=DIRECTION ( 'NONE',  ( -1.000000000000000000, 0.000000000000000000, 0.000000000000000000 ) ) ;
#9541=DIRECTION ( 'NONE',  ( 1.000000000000000000, 0.000000000000000000, 0.000000000000000000 ) ) ;
#9548=LINE ( 'NONE', #5007, #1342 ) ;
#9565=ORIENTED_EDGE ( 'NONE', *, *, #4091, .F. ) ;
#9568=CARTESIAN_POINT ( 'NONE',  ( -0.1749999999999999889, 7.700000000000000178, 1.600000000000000089 ) ) ;
#9581=LINE ( 'NONE', #13747, #6728 ) ;
#9594=LINE ( 'NONE', #8397, #8815 ) ;
#9603=CARTESIAN_POINT ( 'NONE',  ( 2.500000000000000000, 7.299999999999999822, 1.600000000000000089 ) ) ;
#9641=DIRECTION ( 'NONE',  ( 1.000000000000000000, 0.000000000000000000, 0.000000000000000000 ) ) ;
#9643=LINE ( 'NONE', #17031, #14979 ) ;
#9670=VERTEX_POINT ( 'NONE', #1674 ) ;
#9679=ORIENTED_EDGE ( 'NONE', *, *, #3473, .F. ) ;
#9683=ORIENTED_EDGE ( 'NONE', *, *, #9255, .F. ) ;
#9684=VECTOR ( 'NONE', #6611, 1000.000000000000000 ) ;
#9693=EDGE_CURVE ( 'NONE', #5609, #8437, #11661, .T. ) ;
#9729=LINE ( 'NONE', #4164, #4711 ) ;
#9734=ORIENTED_EDGE ( 'NONE', *, *, #9242, .T. ) ;
#9736=ORIENTED_EDGE ( 'NONE', *, *, #13267, .F. ) ;
#9782=ORIENTED_EDGE ( 'NONE', *, *, #2249, .F. ) ;
#9794=EDGE_CURVE ( 'NONE', #8080, #5857, #16088, .T. ) ;
#9806=LINE ( 'NONE', #9989, #8236 ) ;
#9820=CARTESIAN_POINT ( 'NONE',  ( 1.899999999999999911, 9.199999999999999289, 1.600000000000000089 ) ) ;
#9845=ORIENTED_EDGE ( 'NONE', *, *, #9159, .T. ) ;
#9851=ORIENTED_EDGE ( 'NONE', *, *, #5630, .F. ) ;
#9860=CARTESIAN_POINT ( 'NONE',  ( 1.899999999999999911, 9.199999999999999289, 0.5999999999999999778 ) ) ;
#9874=CARTESIAN_POINT ( 'NONE',  ( -2.500000000000000000, 9.199999999999999289, 0.5999999999999999778 ) ) ;
#9884=DIRECTION ( 'NONE',  ( -1.734723475976809806E-16, 1.000000000000000000, 0.000000000000000000 ) ) ;
#9895=LINE ( 'NONE', #14248, #10581 ) ;
#9907=DIRECTION ( 'NONE',  ( 1.000000000000000000, 2.337311630789800155E-16, 2.220446049250309876E-16 ) ) ;
#9908=DIRECTION ( 'NONE',  ( 1.233581138472399909E-16, 6.167905692361979821E-17, -1.000000000000000000 ) ) ;
#9918=LINE ( 'NONE', #11120, #9057 ) ;
#9921=FACE_OUTER_BOUND ( 'NONE', #3001, .T. ) ;
#9933=VERTEX_POINT ( 'NONE', #16894 ) ;
#9989=CARTESIAN_POINT ( 'NONE',  ( 0.1749999999999999889, 9.299999999999998934, 1.600000000000000089 ) ) ;
#9997=LINE ( 'NONE', #7043, #10854 ) ;
#10012=LINE ( 'NONE', #15483, #16805 ) ;
#10034=CARTESIAN_POINT ( 'NONE',  ( -1.899999999999999911, 2.799999999999999822, 1.600000000000000089 ) ) ;
#10035=ORIENTED_EDGE ( 'NONE', *, *, #3473, .T. ) ;
#10048=CARTESIAN_POINT ( 'NONE',  ( 1.899999999999999911, 0.5999999999999999778, 1.600000000000000089 ) ) ;
#10066=DIRECTION ( 'NONE',  ( -2.337311630789800155E-16, 1.000000000000000000, 0.000000000000000000 ) ) ;
#10077=PLANE ( 'NONE',  #3850 ) ;
#10083=ADVANCED_FACE ( 'NONE', ( #15156 ), #2722, .F. ) ;
#10110=LINE ( 'NONE', #3069, #11205 ) ;
#10114=CARTESIAN_POINT ( 'NONE',  ( -0.1749999999999999889, 5.200000000000000178, 0.5999999999999999778 ) ) ;
#10130=VERTEX_POINT ( 'NONE', #4457 ) ;
#10133=CARTESIAN_POINT ( 'NONE',  ( 0.1749999999999999889, 4.299999999999999822, 1.600000000000000089 ) ) ;
#10135=CARTESIAN_POINT ( 'NONE',  ( -0.1749999999999999889, 4.299999999999999822, 0.5999999999999999778 ) ) ;
#10139=PLANE ( 'NONE',  #13804 ) ;
#10151=PLANE ( 'NONE',  #5122 ) ;
#10157=CARTESIAN_POINT ( 'NONE',  ( 0.1749999999999999889, 7.700000000000000178, 0.5999999999999999778 ) ) ;
#10173=DIRECTION ( 'NONE',  ( -1.000000000000000000, -1.908195823574489776E-16, -1.110223024625159992E-16 ) ) ;
#10180=FACE_OUTER_BOUND ( 'NONE', #17809, .T. ) ;
#10193=CARTESIAN_POINT ( 'NONE',  ( 2.500000000000000000, 2.799999999999999822, 0.5999999999999999778 ) ) ;
#10199=DIRECTION ( 'NONE',  ( -0.000000000000000000, 1.000000000000000000, 0.000000000000000000 ) ) ;
#10200=DIRECTION ( 'NONE',  ( 4.440892098500630106E-16, 0.000000000000000000, -1.000000000000000000 ) ) ;
#10222=LINE ( 'NONE', #3290, #12056 ) ;
#10230=CARTESIAN_POINT ( 'NONE',  ( 0.1749999999999999889, 2.700000000000000178, 1.600000000000000089 ) ) ;
#10234=ORIENTED_EDGE ( 'NONE', *, *, #13946, .T. ) ;
#10264=VECTOR ( 'NONE', #13810, 1000.000000000000000 ) ;
#10274=VECTOR ( 'NONE', #8316, 1000.000000000000000 ) ;
#10275=ADVANCED_FACE ( 'NONE', ( #14719 ), #9062, .T. ) ;
#10286=ORIENTED_EDGE ( 'NONE', *, *, #8461, .F. ) ;
#10292=VERTEX_POINT ( 'NONE', #14463 ) ;
#10302=ORIENTED_EDGE ( 'NONE', *, *, #3351, .F. ) ;
#10307=CARTESIAN_POINT ( 'NONE',  ( 1.899999999999999911, 9.199999999999999289, 1.600000000000000089 ) ) ;
#10323=EDGE_LOOP ( 'NONE', ( #9845, #13499, #5775, #16971 ) ) ;
#10333=ORIENTED_EDGE ( 'NONE', *, *, #3351, .T. ) ;
#10338=EDGE_LOOP ( 'NONE', ( #15698, #6860, #15301, #5896 ) ) ;
#10351=LINE ( 'NONE', #1845, #7282 ) ;
#10386=CARTESIAN_POINT ( 'NONE',  ( -2.500000000000000000, 7.299999999999999822, 1.600000000000000089 ) ) ;
#10395=EDGE_CURVE ( 'NONE', #10948, #9933, #742, .T. ) ;
#10396=VERTEX_POINT ( 'NONE', #1031 ) ;
#10399=DIRECTION ( 'NONE',  ( 1.168655815394900078E-16, -1.000000000000000000, -5.843279076974510248E-17 ) ) ;
#10410=ORIENTED_EDGE ( 'NONE', *, *, #17839, .T. ) ;
#10419=CARTESIAN_POINT ( 'NONE',  ( 0.1749999999999999889, 6.799999999999999822, 1.600000000000000089 ) ) ;
#10435=DIRECTION ( 'NONE',  ( 1.000000000000000000, 0.000000000000000000, 0.000000000000000000 ) ) ;
#10441=DIRECTION ( 'NONE',  ( -1.734723475976809806E-16, 1.000000000000000000, 0.000000000000000000 ) ) ;
#10448=LINE ( 'NONE', #558, #11749 ) ;
#10463=ORIENTED_EDGE ( 'NONE', *, *, #3584, .F. ) ;
#10470=ADVANCED_FACE ( 'NONE', ( #9456 ), #10941, .T. ) ;
#10472=( GEOMETRIC_REPRESENTATION_CONTEXT ( 3 ) GLOBAL_UNCERTAINTY_ASSIGNED_CONTEXT ( ( #12511 ) ) GLOBAL_UNIT_ASSIGNED_CONTEXT ( ( #2497, #9329, #13704 ) ) REPRESENTATION_CONTEXT ( 'NONE', 'WORKASPACE' ) );
#10496=ORIENTED_EDGE ( 'NONE', *, *, #5521, .T. ) ;
#10497=FACE_OUTER_BOUND ( 'NONE', #10792, .T. ) ;
#10500=ORIENTED_EDGE ( 'NONE', *, *, #16602, .F. ) ;
#10505=VERTEX_POINT ( 'NONE', #9820 ) ;
#10508=CARTESIAN_POINT ( 'NONE',  ( 0.1749999999999999889, 7.700000000000000178, 1.600000000000000089 ) ) ;
#10540=DIRECTION ( 'NONE',  ( 1.734723475976809806E-16, -1.000000000000000000, 0.000000000000000000 ) ) ;
#10547=VECTOR ( 'NONE', #10435, 1000.000000000000000 ) ;
#10552=LINE ( 'NONE', #9166, #7813 ) ;
#10570=EDGE_CURVE ( 'NONE', #10292, #13656, #9729, .T. ) ;
#10581=VECTOR ( 'NONE', #11193, 1000.000000000000000 ) ;
#10597=ORIENTED_EDGE ( 'NONE', *, *, #12698, .F. ) ;
#10611=ORIENTED_EDGE ( 'NONE', *, *, #17839, .F. ) ;
#10614=CARTESIAN_POINT ( 'NONE',  ( -0.1749999999999999889, 6.799999999999999822, 0.5999999999999999778 ) ) ;
#10624=DIRECTION ( 'NONE',  ( 1.110223024625159992E-16, 0.000000000000000000, -1.000000000000000000 ) ) ;
#10661=CARTESIAN_POINT ( 'NONE',  ( 2.500000000000000000, 9.199999999999999289, 1.600000000000000089 ) ) ;
#10665=DIRECTION ( 'NONE',  ( 0.000000000000000000, -1.000000000000000000, 0.000000000000000000 ) ) ;
#10666=ORIENTED_EDGE ( 'NONE', *, *, #5956, .F. ) ;
#10674=DIRECTION ( 'NONE',  ( 1.000000000000000000, 1.908195823574489776E-16, 1.110223024625159992E-16 ) ) ;
#10684=LINE ( 'NONE', #10869, #10983 ) ;
#10687=ORIENTED_EDGE ( 'NONE', *, *, #6329, .T. ) ;
#10719=CARTESIAN_POINT ( 'NONE',  ( -1.899999999999999911, 9.199999999999999289, 1.600000000000000089 ) ) ;
#10738=CARTESIAN_POINT ( 'NONE',  ( 0.1749999999999999889, 9.299999999999998934, 0.5999999999999999778 ) ) ;
#10768=ORIENTED_EDGE ( 'NONE', *, *, #11513, .T. ) ;
#10772=LINE ( 'NONE', #15421, #7075 ) ;
#10782=PLANE ( 'NONE',  #5525 ) ;
#10792=EDGE_LOOP ( 'NONE', ( #14441, #700, #4286, #5059 ) ) ;
#10793=LINE ( 'NONE', #11907, #8200 ) ;
#10797=EDGE_LOOP ( 'NONE', ( #17833, #9530, #10916, #1068 ) ) ;
#10818=PRODUCT_DEFINITION_SHAPE ( 'NONE', 'NONE',  #13304 ) ;
#10819=SURFACE_SIDE_STYLE ('',( #13612 ) ) ;
#10827=ADVANCED_FACE ( 'NONE', ( #1925 ), #4878, .T. ) ;
#10839=ORIENTED_EDGE ( 'NONE', *, *, #2035, .T. ) ;
#10840=CARTESIAN_POINT ( 'NONE',  ( -0.1749999999999999889, 7.700000000000000178, 1.600000000000000089 ) ) ;
#10850=CARTESIAN_POINT ( 'NONE',  ( 0.1749999999999999889, 5.200000000000000178, 1.600000000000000089 ) ) ;
#10854=VECTOR ( 'NONE', #15662, 1000.000000000000000 ) ;
#10869=CARTESIAN_POINT ( 'NONE',  ( 2.500000000000000000, 10.00000000000000000, 1.600000000000000089 ) ) ;
#10878=VECTOR ( 'NONE', #16264, 1000.000000000000000 ) ;
#10879=DIRECTION ( 'NONE',  ( 0.000000000000000000, -8.217301096052200103E-32, -1.000000000000000000 ) ) ;
#10887=DIRECTION ( 'NONE',  ( -1.000000000000000000, 0.000000000000000000, 0.000000000000000000 ) ) ;
#10916=ORIENTED_EDGE ( 'NONE', *, *, #14700, .F. ) ;
#10934=DIRECTION ( 'NONE',  ( -0.000000000000000000, 1.000000000000000000, 0.000000000000000000 ) ) ;
#10941=PLANE ( 'NONE',  #572 ) ;
#10948=VERTEX_POINT ( 'NONE', #11005 ) ;
#10951=ORIENTED_EDGE ( 'NONE', *, *, #5871, .T. ) ;
#10983=VECTOR ( 'NONE', #17786, 1000.000000000000000 ) ;
#11005=CARTESIAN_POINT ( 'NONE',  ( 1.899999999999999911, 2.000000000000000000, 0.5999999999999999778 ) ) ;
#11011=LINE ( 'NONE', #8147, #5881 ) ;
#11012=ORIENTED_EDGE ( 'NONE', *, *, #2125, .T. ) ;
#11021=FACE_OUTER_BOUND ( 'NONE', #1219, .T. ) ;
#11039=LINE ( 'NONE', #16688, #6132 ) ;
#11071=AXIS2_PLACEMENT_3D ( 'NONE', #7494, #11847, #10441 ) ;
#11082=CARTESIAN_POINT ( 'NONE',  ( -1.899999999999999911, 9.199999999999999289, 0.5999999999999999778 ) ) ;
#11106=CARTESIAN_POINT ( 'NONE',  ( 1.899999999999999911, 4.700000000000000178, 0.5999999999999999778 ) ) ;
#11120=CARTESIAN_POINT ( 'NONE',  ( 0.1749999999999999889, 6.799999999999999822, 1.600000000000000089 ) ) ;
#11121=LINE ( 'NONE', #15679, #4597 ) ;
#11150=ORIENTED_EDGE ( 'NONE', *, *, #18289, .T. ) ;
#11152=VECTOR ( 'NONE', #1595, 1000.000000000000000 ) ;
#11154=AXIS2_PLACEMENT_3D ( 'NONE', #288, #10173, #15837 ) ;
#11181=AXIS2_PLACEMENT_3D ( 'NONE', #14079, #114, #8631 ) ;
#11191=CARTESIAN_POINT ( 'NONE',  ( 0.000000000000000000, 0.000000000000000000, 0.000000000000000000 ) ) ;
#11193=DIRECTION ( 'NONE',  ( 1.110223024625159992E-16, 0.000000000000000000, -1.000000000000000000 ) ) ;
#11201=PLANE ( 'NONE',  #13519 ) ;
#11205=VECTOR ( 'NONE', #8805, 1000.000000000000000 ) ;
#11208=FACE_BOUND ( 'NONE', #7082, .T. ) ;
#11221=DIRECTION ( 'NONE',  ( 1.110223024625159992E-16, 0.000000000000000000, -1.000000000000000000 ) ) ;
#11284=LINE ( 'NONE', #17008, #2638 ) ;
#11286=ORIENTED_EDGE ( 'NONE', *, *, #2249, .T. ) ;
#11306=LINE ( 'NONE', #12792, #13554 ) ;
#11330=CARTESIAN_POINT ( 'NONE',  ( 2.500000000000000000, 10.00000000000000000, 1.600000000000000089 ) ) ;
#11344=DIRECTION ( 'NONE',  ( 0.000000000000000000, 0.000000000000000000, -1.000000000000000000 ) ) ;
#11350=ORIENTED_EDGE ( 'NONE', *, *, #17159, .F. ) ;
#11359=CARTESIAN_POINT ( 'NONE',  ( 2.500000000000000000, 4.700000000000000178, 1.600000000000000089 ) ) ;
#11431=ADVANCED_FACE ( 'NONE', ( #4418 ), #10077, .F. ) ;
#11432=AXIS2_PLACEMENT_3D ( 'NONE', #3349, #10934, #9541 ) ;
#11434=DIRECTION ( 'NONE',  ( 1.734723475976809806E-16, -1.000000000000000000, 0.000000000000000000 ) ) ;
#11442=VECTOR ( 'NONE', #15471, 1000.000000000000000 ) ;
#11463=VERTEX_POINT ( 'NONE', #10419 ) ;
#11471=CARTESIAN_POINT ( 'NONE',  ( -2.500000000000000000, 2.799999999999999822, 1.600000000000000089 ) ) ;
#11476=PLANE ( 'NONE',  #3482 ) ;
#11500=( GEOMETRIC_REPRESENTATION_CONTEXT ( 3 ) GLOBAL_UNCERTAINTY_ASSIGNED_CONTEXT ( ( #15300 ) ) GLOBAL_UNIT_ASSIGNED_CONTEXT ( ( #1243, #5322, #16613 ) ) REPRESENTATION_CONTEXT ( 'NONE', 'WORKASPACE' ) );
#11513=EDGE_CURVE ( 'NONE', #9201, #10948, #16440, .T. ) ;
#11524=LINE ( 'NONE', #4474, #4919 ) ;
#11555=DIRECTION ( 'NONE',  ( 1.000000000000000000, 0.000000000000000000, 0.000000000000000000 ) ) ;
#11568=ORIENTED_EDGE ( 'NONE', *, *, #6540, .T. ) ;
#11583=ORIENTED_EDGE ( 'NONE', *, *, #2705, .T. ) ;
#11587=ORIENTED_EDGE ( 'NONE', *, *, #5871, .F. ) ;
#11606=CARTESIAN_POINT ( 'NONE',  ( 2.500000000000000000, 7.299999999999999822, 0.5999999999999999778 ) ) ;
#11607=LINE ( 'NONE', #9348, #15346 ) ;
#11619=DIRECTION ( 'NONE',  ( -2.220446049250309876E-16, 0.000000000000000000, 1.000000000000000000 ) ) ;
#11633=ORIENTED_EDGE ( 'NONE', *, *, #3297, .T. ) ;
#11661=LINE ( 'NONE', #2025, #6460 ) ;
#11673=CARTESIAN_POINT ( 'NONE',  ( -1.899999999999999911, 4.700000000000000178, 1.600000000000000089 ) ) ;
#11749=VECTOR ( 'NONE', #14352, 1000.000000000000000 ) ;
#11761=VERTEX_POINT ( 'NONE', #3191 ) ;
#11769=CARTESIAN_POINT ( 'NONE',  ( 2.500000000000000000, 2.799999999999999822, 1.600000000000000089 ) ) ;
#11770=EDGE_CURVE ( 'NONE', #15397, #1059, #7189, .T. ) ;
#11804=ORIENTED_EDGE ( 'NONE', *, *, #16295, .F. ) ;
#11847=DIRECTION ( 'NONE',  ( 1.000000000000000000, 1.734723475976809806E-16, 1.110223024625159992E-16 ) ) ;
#11853=ORIENTED_EDGE ( 'NONE', *, *, #5521, .F. ) ;
#11907=CARTESIAN_POINT ( 'NONE',  ( 2.500000000000000000, 10.00000000000000000, 1.600000000000000089 ) ) ;
#11911=VERTEX_POINT ( 'NONE', #13555 ) ;
#11940=PLANE ( 'NONE',  #6142 ) ;
#11954=ORIENTED_EDGE ( 'NONE', *, *, #4151, .T. ) ;
#11987=CARTESIAN_POINT ( 'NONE',  ( -1.899999999999999911, 2.000000000000000000, 0.5999999999999999778 ) ) ;
#11992=LINE ( 'NONE', #17712, #15043 ) ;
#11996=PLANE ( 'NONE',  #2325 ) ;
#12019=CARTESIAN_POINT ( 'NONE',  ( -1.899999999999999911, 0.5999999999999999778, 1.600000000000000089 ) ) ;
#12056=VECTOR ( 'NONE', #15987, 1000.000000000000000 ) ;
#12097=ORIENTED_EDGE ( 'NONE', *, *, #12654, .F. ) ;
#12119=CARTESIAN_POINT ( 'NONE',  ( -2.500000000000000000, 4.700000000000000178, 0.5999999999999999778 ) ) ;
#12126=LINE ( 'NONE', #12214, #12496 ) ;
#12132=EDGE_CURVE ( 'NONE', #6275, #6036, #6077, .T. ) ;
#12147=LINE ( 'NONE', #13801, #5461 ) ;
#12150=ORIENTED_EDGE ( 'NONE', *, *, #5296, .T. ) ;
#12165=VERTEX_POINT ( 'NONE', #3472 ) ;
#12181=ORIENTED_EDGE ( 'NONE', *, *, #7917, .F. ) ;
#12184=EDGE_CURVE ( 'NONE', #14849, #15379, #9120, .T. ) ;
#12189=DIRECTION ( 'NONE',  ( -1.000000000000000000, -1.168655815394900078E-16, -1.168655815394900078E-16 ) ) ;
#12197=VERTEX_POINT ( 'NONE', #17360 ) ;
#12214=CARTESIAN_POINT ( 'NONE',  ( 1.899999999999999911, 0.5999999999999999778, 0.5999999999999999778 ) ) ;
#12238=ORIENTED_EDGE ( 'NONE', *, *, #12855, .T. ) ;
#12253=ORIENTED_EDGE ( 'NONE', *, *, #9693, .F. ) ;
#12255=VERTEX_POINT ( 'NONE', #6338 ) ;
#12257=DIRECTION ( 'NONE',  ( -1.000000000000000000, 0.000000000000000000, 0.000000000000000000 ) ) ;
#12294=CARTESIAN_POINT ( 'NONE',  ( -1.899999999999999911, 2.000000000000000000, 1.600000000000000089 ) ) ;
#12295=CARTESIAN_POINT ( 'NONE',  ( -2.500000000000000000, 7.299999999999999822, 1.600000000000000089 ) ) ;
#12305=ORIENTED_EDGE ( 'NONE', *, *, #14060, .T. ) ;
#12312=VECTOR ( 'NONE', #6479, 1000.000000000000000 ) ;
#12316=DIRECTION ( 'NONE',  ( -1.000000000000000000, 0.000000000000000000, -1.850371707708589879E-16 ) ) ;
#12337=VECTOR ( 'NONE', #2595, 1000.000000000000000 ) ;
#12347=ORIENTED_EDGE ( 'NONE', *, *, #11770, .T. ) ;
#12381=FACE_OUTER_BOUND ( 'NONE', #4255, .T. ) ;
#12408=DIRECTION ( 'NONE',  ( -1.000000000000000000, 0.000000000000000000, 0.000000000000000000 ) ) ;
#12429=LINE ( 'NONE', #13640, #10264 ) ;
#12432=DIRECTION ( 'NONE',  ( 2.337311630789800155E-16, -1.000000000000000000, -1.168655815394900078E-16 ) ) ;
#12433=VECTOR ( 'NONE', #11434, 1000.000000000000000 ) ;
#12470=ORIENTED_EDGE ( 'NONE', *, *, #2705, .F. ) ;
#12477=DIRECTION ( 'NONE',  ( 0.000000000000000000, 0.000000000000000000, -1.000000000000000000 ) ) ;
#12496=VECTOR ( 'NONE', #8140, 1000.000000000000000 ) ;
#12511=UNCERTAINTY_MEASURE_WITH_UNIT (LENGTH_MEASURE( 1.000000000000000082E-05 ), #2497, 'distance_accuracy_value', 'NONE');
#12527=DIRECTION ( 'NONE',  ( 1.000000000000000000, 0.000000000000000000, 0.000000000000000000 ) ) ;
#12528=VERTEX_POINT ( 'NONE', #9874 ) ;
#12534=ORIENTED_EDGE ( 'NONE', *, *, #16868, .F. ) ;
#12541=CARTESIAN_POINT ( 'NONE',  ( 0.1749999999999999889, 7.700000000000000178, 0.5999999999999999778 ) ) ;
#12555=ORIENTED_EDGE ( 'NONE', *, *, #5910, .T. ) ;
#12562=EDGE_CURVE ( 'NONE', #9265, #16145, #7459, .T. ) ;
#12566=ORIENTED_EDGE ( 'NONE', *, *, #8135, .T. ) ;
#12604=DIRECTION ( 'NONE',  ( -1.168655815394900078E-16, 1.000000000000000000, 0.000000000000000000 ) ) ;
#12617=ORIENTED_EDGE ( 'NONE', *, *, #9794, .F. ) ;
#12654=EDGE_CURVE ( 'NONE', #2568, #8419, #678, .T. ) ;
#12657=LINE ( 'NONE', #18278, #16471 ) ;
#12693=DIRECTION ( 'NONE',  ( -2.337311630789800155E-16, 1.000000000000000000, 0.000000000000000000 ) ) ;
#12698=EDGE_CURVE ( 'NONE', #18021, #2376, #10684, .T. ) ;
#12733=ORIENTED_EDGE ( 'NONE', *, *, #13199, .T. ) ;
#12792=CARTESIAN_POINT ( 'NONE',  ( 1.899999999999999911, 11.40000000000000036, 1.600000000000000089 ) ) ;
#12805=VECTOR ( 'NONE', #6003, 1000.000000000000000 ) ;
#12820=EDGE_CURVE ( 'NONE', #8080, #8437, #13441, .T. ) ;
#12821=LINE ( 'NONE', #10307, #14663 ) ;
#12838=CARTESIAN_POINT ( 'NONE',  ( -0.1749999999999999889, 7.700000000000000178, 0.5999999999999999778 ) ) ;
#12841=ORIENTED_EDGE ( 'NONE', *, *, #5686, .T. ) ;
#12843=CARTESIAN_POINT ( 'NONE',  ( 1.899999999999999911, 2.799999999999999822, 1.600000000000000089 ) ) ;
#12855=EDGE_CURVE ( 'NONE', #5857, #5609, #17675, .T. ) ;
#12913=VECTOR ( 'NONE', #1532, 1000.000000000000000 ) ;
#12920=CARTESIAN_POINT ( 'NONE',  ( 1.899999999999999911, 7.299999999999999822, 1.600000000000000089 ) ) ;
#12960=EDGE_LOOP ( 'NONE', ( #4248, #17356, #13301, #16881 ) ) ;
#12961=VECTOR ( 'NONE', #938, 1000.000000000000000 ) ;
#12964=PLANE ( 'NONE',  #11154 ) ;
#12997=ORIENTED_EDGE ( 'NONE', *, *, #7560, .T. ) ;
#13008=LINE ( 'NONE', #17852, #1092 ) ;
#13020=LINE ( 'NONE', #6061, #4634 ) ;
#13026=CARTESIAN_POINT ( 'NONE',  ( -2.500000000000000000, 2.000000000000000000, 1.600000000000000089 ) ) ;
#13044=DIRECTION ( 'NONE',  ( 0.000000000000000000, -1.000000000000000000, -1.387778780781439759E-16 ) ) ;
#13050=EDGE_LOOP ( 'NONE', ( #1472, #1833, #9736, #6341 ) ) ;
#13076=ORIENTED_EDGE ( 'NONE', *, *, #14580, .F. ) ;
#13107=EDGE_CURVE ( 'NONE', #16569, #15379, #8136, .T. ) ;
#13116=VERTEX_POINT ( 'NONE', #15097 ) ;
#13120=CARTESIAN_POINT ( 'NONE',  ( -0.1749999999999999889, 7.700000000000000178, 1.600000000000000089 ) ) ;
#13141=CARTESIAN_POINT ( 'NONE',  ( -0.1749999999999999889, 5.200000000000000178, 0.5999999999999999778 ) ) ;
#13188=CARTESIAN_POINT ( 'NONE',  ( -2.500000000000000000, 9.199999999999999289, 1.600000000000000089 ) ) ;
#13199=EDGE_CURVE ( 'NONE', #1946, #16101, #6354, .T. ) ;
#13227=CARTESIAN_POINT ( 'NONE',  ( 1.899999999999999911, 4.700000000000000178, 1.600000000000000089 ) ) ;
#13237=AXIS2_PLACEMENT_3D ( 'NONE', #17893, #6529, #891 ) ;
#13238=LINE ( 'NONE', #15843, #16174 ) ;
#13262=ORIENTED_EDGE ( 'NONE', *, *, #6495, .F. ) ;
#13267=EDGE_CURVE ( 'NONE', #9279, #14793, #2572, .T. ) ;
#13273=ORIENTED_EDGE ( 'NONE', *, *, #16282, .T. ) ;
#13291=DIRECTION ( 'NONE',  ( -1.000000000000000000, -2.337311630789800155E-16, -2.220446049250309876E-16 ) ) ;
#13301=ORIENTED_EDGE ( 'NONE', *, *, #2590, .T. ) ;
#13304=PRODUCT_DEFINITION ( 'UNKNOWN', '', #7383, #8262 ) ;
#13333=VECTOR ( 'NONE', #16499, 1000.000000000000000 ) ;
#13344=EDGE_LOOP ( 'NONE', ( #11568, #13824, #9273, #2243 ) ) ;
#13381=ORIENTED_EDGE ( 'NONE', *, *, #761, .F. ) ;
#13382=LINE ( 'NONE', #9206, #4340 ) ;
#13411=ORIENTED_EDGE ( 'NONE', *, *, #2125, .F. ) ;
#13416=ORIENTED_EDGE ( 'NONE', *, *, #7216, .T. ) ;
#13419=FACE_OUTER_BOUND ( 'NONE', #16525, .T. ) ;
#13422=DIRECTION ( 'NONE',  ( 1.000000000000000000, 0.000000000000000000, 0.000000000000000000 ) ) ;
#13434=COLOUR_RGB ( '', 0.31764706, 0.68627451, 0.89019608) ;
#13435=VERTEX_POINT ( 'NONE', #12843 ) ;
#13441=LINE ( 'NONE', #10850, #13333 ) ;
#13446=DIRECTION ( 'NONE',  ( 4.440892098500630106E-16, 0.000000000000000000, -1.000000000000000000 ) ) ;
#13458=ORIENTED_EDGE ( 'NONE', *, *, #17578, .F. ) ;
#13499=ORIENTED_EDGE ( 'NONE', *, *, #12562, .T. ) ;
#13515=VECTOR ( 'NONE', #2193, 1000.000000000000000 ) ;
#13519=AXIS2_PLACEMENT_3D ( 'NONE', #8422, #5737, #17015 ) ;
#13525=LINE ( 'NONE', #2333, #4947 ) ;
#13545=CARTESIAN_POINT ( 'NONE',  ( 2.500000000000000000, 7.299999999999999822, 0.5999999999999999778 ) ) ;
#13550=VECTOR ( 'NONE', #10540, 1000.000000000000000 ) ;
#13554=VECTOR ( 'NONE', #8532, 1000.000000000000000 ) ;
#13555=CARTESIAN_POINT ( 'NONE',  ( -1.899999999999999911, 7.299999999999999822, 1.600000000000000089 ) ) ;
#13581=CARTESIAN_POINT ( 'NONE',  ( -2.500000000000000000, 4.700000000000000178, 1.600000000000000089 ) ) ;
#13591=VERTEX_POINT ( 'NONE', #6163 ) ;
#13612=SURFACE_STYLE_FILL_AREA ( #7966 ) ;
#13620=ADVANCED_FACE ( 'NONE', ( #16157 ), #3742, .T. ) ;
#13628=VECTOR ( 'NONE', #9410, 1000.000000000000000 ) ;
#13640=CARTESIAN_POINT ( 'NONE',  ( -2.500000000000000000, 7.299999999999999822, 0.5999999999999999778 ) ) ;
#13642=DIRECTION ( 'NONE',  ( 1.110223024625159992E-16, 0.000000000000000000, -1.000000000000000000 ) ) ;
#13643=CARTESIAN_POINT ( 'NONE',  ( -1.899999999999999911, 11.40000000000000036, 1.600000000000000089 ) ) ;
#13648=ORIENTED_EDGE ( 'NONE', *, *, #8312, .F. ) ;
#13656=VERTEX_POINT ( 'NONE', #11606 ) ;
#13660=FACE_OUTER_BOUND ( 'NONE', #15226, .T. ) ;
#13667=DIRECTION ( 'NONE',  ( -1.000000000000000000, 0.000000000000000000, 0.000000000000000000 ) ) ;
#13672=DIRECTION ( 'NONE',  ( -4.440892098500630106E-16, 0.000000000000000000, 1.000000000000000000 ) ) ;
#13704=( NAMED_UNIT ( * ) SI_UNIT ( $, .STERADIAN. ) SOLID_ANGLE_UNIT ( ) );
#13715=CARTESIAN_POINT ( 'NONE',  ( -2.500000000000000000, 2.000000000000000000, 1.600000000000000089 ) ) ;
#13717=ORIENTED_EDGE ( 'NONE', *, *, #12855, .F. ) ;
#13726=CARTESIAN_POINT ( 'NONE',  ( -0.1749999999999999889, 9.299999999999998934, 1.600000000000000089 ) ) ;
#13737=DIRECTION ( 'NONE',  ( 1.168655815394900078E-16, -1.000000000000000000, -1.110223024625159992E-16 ) ) ;
#13747=CARTESIAN_POINT ( 'NONE',  ( 2.500000000000000000, 9.199999999999999289, 1.600000000000000089 ) ) ;
#13759=LINE ( 'NONE', #2393, #13515 ) ;
#13764=CARTESIAN_POINT ( 'NONE',  ( 2.500000000000000000, 2.799999999999999822, 0.5999999999999999778 ) ) ;
#13775=LINE ( 'NONE', #6745, #2156 ) ;
#13784=ORIENTED_EDGE ( 'NONE', *, *, #3073, .F. ) ;
#13800=ORIENTED_EDGE ( 'NONE', *, *, #16513, .T. ) ;
#13801=CARTESIAN_POINT ( 'NONE',  ( 0.1749999999999999889, 4.299999999999999822, 1.600000000000000089 ) ) ;
#13802=ORIENTED_EDGE ( 'NONE', *, *, #6495, .T. ) ;
#13804=AXIS2_PLACEMENT_3D ( 'NONE', #1457, #16992, #4305 ) ;
#13810=DIRECTION ( 'NONE',  ( 1.000000000000000000, 0.000000000000000000, 0.000000000000000000 ) ) ;
#13813=DIRECTION ( 'NONE',  ( 1.000000000000000000, 0.000000000000000000, 1.168655815394900078E-16 ) ) ;
#13823=EDGE_CURVE ( 'NONE', #15295, #11463, #11524, .T. ) ;
#13824=ORIENTED_EDGE ( 'NONE', *, *, #5352, .T. ) ;
#13840=AXIS2_PLACEMENT_3D ( 'NONE', #10508, #704, #17620 ) ;
#13850=EDGE_CURVE ( 'NONE', #11463, #4854, #9918, .T. ) ;
#13881=PLANE ( 'NONE',  #7868 ) ;
#13901=ORIENTED_EDGE ( 'NONE', *, *, #17159, .T. ) ;
#13912=DIRECTION ( 'NONE',  ( 1.908195823574489776E-16, -1.000000000000000000, -6.938893903907229610E-17 ) ) ;
#13926=VECTOR ( 'NONE', #9001, 1000.000000000000000 ) ;
#13946=EDGE_CURVE ( 'NONE', #17729, #6294, #1308, .T. ) ;
#13971=CARTESIAN_POINT ( 'NONE',  ( -2.500000000000000000, 4.700000000000000178, 1.600000000000000089 ) ) ;
#14001=EDGE_CURVE ( 'NONE', #5569, #9670, #13238, .T. ) ;
#14008=CARTESIAN_POINT ( 'NONE',  ( -2.500000000000000000, 2.000000000000000000, 1.600000000000000089 ) ) ;
#14022=ADVANCED_FACE ( 'NONE', ( #4714 ), #7684, .T. ) ;
#14024=CARTESIAN_POINT ( 'NONE',  ( 0.1749999999999999889, 2.700000000000000178, 1.600000000000000089 ) ) ;
#14054=CARTESIAN_POINT ( 'NONE',  ( -2.500000000000000000, 10.00000000000000000, 1.600000000000000089 ) ) ;
#14059=CARTESIAN_POINT ( 'NONE',  ( -1.899999999999999911, 10.00000000000000000, 0.5999999999999999778 ) ) ;
#14060=EDGE_CURVE ( 'NONE', #6586, #17492, #10448, .T. ) ;
#14079=CARTESIAN_POINT ( 'NONE',  ( 2.500000000000000000, 4.700000000000000178, 1.600000000000000089 ) ) ;
#14107=DIRECTION ( 'NONE',  ( 2.337311630789800155E-16, -1.000000000000000000, -1.168655815394900078E-16 ) ) ;
#14112=VECTOR ( 'NONE', #6521, 1000.000000000000000 ) ;
#14113=ORIENTED_EDGE ( 'NONE', *, *, #2940, .T. ) ;
#14151=ORIENTED_EDGE ( 'NONE', *, *, #13823, .F. ) ;
#14156=LINE ( 'NONE', #1477, #5866 ) ;
#14164=LINE ( 'NONE', #1570, #15011 ) ;
#14165=CARTESIAN_POINT ( 'NONE',  ( 1.899999999999999911, 11.40000000000000036, 1.600000000000000089 ) ) ;
#14170=CARTESIAN_POINT ( 'NONE',  ( 1.899999999999999911, 10.00000000000000000, 1.600000000000000089 ) ) ;
#14180=EDGE_CURVE ( 'NONE', #1059, #9279, #14164, .T. ) ;
#14207=ORIENTED_EDGE ( 'NONE', *, *, #8347, .F. ) ;
#14215=LINE ( 'NONE', #10048, #8800 ) ;
#14231=VECTOR ( 'NONE', #3618, 1000.000000000000000 ) ;
#14239=ADVANCED_FACE ( 'NONE', ( #14688 ), #6084, .T. ) ;
#14248=CARTESIAN_POINT ( 'NONE',  ( -0.1749999999999999889, 6.799999999999999822, 1.600000000000000089 ) ) ;
#14257=FACE_OUTER_BOUND ( 'NONE', #4962, .T. ) ;
#14290=ORIENTED_EDGE ( 'NONE', *, *, #12654, .T. ) ;
#14352=DIRECTION ( 'NONE',  ( 1.000000000000000000, 0.000000000000000000, 0.000000000000000000 ) ) ;
#14361=DIRECTION ( 'NONE',  ( -1.734723475976809806E-16, 1.000000000000000000, 0.000000000000000000 ) ) ;
#14371=SHAPE_DEFINITION_REPRESENTATION ( #10818, #5932 ) ;
#14374=EDGE_CURVE ( 'NONE', #7912, #3782, #8871, .T. ) ;
#14393=LINE ( 'NONE', #334, #7052 ) ;
#14401=VECTOR ( 'NONE', #1358, 1000.000000000000000 ) ;
#14414=LINE ( 'NONE', #13120, #7493 ) ;
#14419=VECTOR ( 'NONE', #8585, 1000.000000000000000 ) ;
#14434=AXIS2_PLACEMENT_3D ( 'NONE', #7647, #13291, #518 ) ;
#14441=ORIENTED_EDGE ( 'NONE', *, *, #3034, .T. ) ;
#14454=DIRECTION ( 'NONE',  ( 0.000000000000000000, -1.000000000000000000, -6.167905692361979821E-17 ) ) ;
#14463=CARTESIAN_POINT ( 'NONE',  ( 1.899999999999999911, 7.299999999999999822, 0.5999999999999999778 ) ) ;
#14515=ORIENTED_EDGE ( 'NONE', *, *, #15713, .F. ) ;
#14528=VERTEX_POINT ( 'NONE', #3862 ) ;
#14562=CARTESIAN_POINT ( 'NONE',  ( 1.899999999999999911, 10.00000000000000000, 1.600000000000000089 ) ) ;
#14568=VERTEX_POINT ( 'NONE', #3763 ) ;
#14580=EDGE_CURVE ( 'NONE', #17990, #9201, #2563, .T. ) ;
#14585=ORIENTED_EDGE ( 'NONE', *, *, #12820, .T. ) ;
#14589=PLANE ( 'NONE',  #14434 ) ;
#14631=ORIENTED_EDGE ( 'NONE', *, *, #3431, .T. ) ;
#14663=VECTOR ( 'NONE', #15971, 1000.000000000000000 ) ;
#14688=FACE_OUTER_BOUND ( 'NONE', #10797, .T. ) ;
#14700=EDGE_CURVE ( 'NONE', #8906, #17990, #16645, .T. ) ;
#14701=LINE ( 'NONE', #13227, #135 ) ;
#14710=CARTESIAN_POINT ( 'NONE',  ( 2.500000000000000000, 2.000000000000000000, 1.600000000000000089 ) ) ;
#14715=VECTOR ( 'NONE', #8845, 1000.000000000000000 ) ;
#14719=FACE_OUTER_BOUND ( 'NONE', #13344, .T. ) ;
#14732=AXIS2_PLACEMENT_3D ( 'NONE', #7825, #3460, #9109 ) ;
#14737=CARTESIAN_POINT ( 'NONE',  ( 2.500000000000000000, 2.000000000000000000, 1.600000000000000089 ) ) ;
#14780=ORIENTED_EDGE ( 'NONE', *, *, #2868, .T. ) ;
#14789=EDGE_CURVE ( 'NONE', #12528, #17729, #10222, .T. ) ;
#14793=VERTEX_POINT ( 'NONE', #17247 ) ;
#14808=CARTESIAN_POINT ( 'NONE',  ( -0.1749999999999999889, 9.299999999999998934, 0.5999999999999999778 ) ) ;
#14825=ORIENTED_EDGE ( 'NONE', *, *, #13107, .F. ) ;
#14841=LINE ( 'NONE', #1956, #3155 ) ;
#14849=VERTEX_POINT ( 'NONE', #12838 ) ;
#14871=DIRECTION ( 'NONE',  ( 2.220446049250309876E-16, 0.000000000000000000, -1.000000000000000000 ) ) ;
#14876=ORIENTED_EDGE ( 'NONE', *, *, #15750, .F. ) ;
#14879=FACE_OUTER_BOUND ( 'NONE', #3710, .T. ) ;
#14890=LINE ( 'NONE', #12119, #6478 ) ;
#14917=DIRECTION ( 'NONE',  ( 0.000000000000000000, 0.000000000000000000, -1.000000000000000000 ) ) ;
#14920=EDGE_CURVE ( 'NONE', #17492, #12197, #15637, .T. ) ;
#14930=EDGE_CURVE ( 'NONE', #1590, #16145, #7197, .T. ) ;
#14932=ADVANCED_FACE ( 'NONE', ( #8852 ), #5977, .T. ) ;
#14949=ORIENTED_EDGE ( 'NONE', *, *, #15508, .T. ) ;
#14970=CARTESIAN_POINT ( 'NONE',  ( 2.500000000000000000, 2.000000000000000000, 0.5999999999999999778 ) ) ;
#14977=PLANE ( 'NONE',  #3430 ) ;
#14978=ORIENTED_EDGE ( 'NONE', *, *, #4732, .T. ) ;
#14979=VECTOR ( 'NONE', #12604, 1000.000000000000000 ) ;
#14989=DIRECTION ( 'NONE',  ( 0.000000000000000000, 1.000000000000000000, 0.000000000000000000 ) ) ;
#15004=VECTOR ( 'NONE', #10200, 1000.000000000000000 ) ;
#15011=VECTOR ( 'NONE', #12408, 1000.000000000000000 ) ;
#15031=FACE_OUTER_BOUND ( 'NONE', #8732, .T. ) ;
#15043=VECTOR ( 'NONE', #13667, 1000.000000000000000 ) ;
#15070=CARTESIAN_POINT ( 'NONE',  ( 1.899999999999999911, 10.00000000000000000, 1.600000000000000089 ) ) ;
#15075=CARTESIAN_POINT ( 'NONE',  ( 0.1749999999999999889, 6.799999999999999822, 1.600000000000000089 ) ) ;
#15097=CARTESIAN_POINT ( 'NONE',  ( -0.1749999999999999889, 6.799999999999999822, 0.5999999999999999778 ) ) ;
#15155=FACE_OUTER_BOUND ( 'NONE', #4851, .T. ) ;
#15156=FACE_OUTER_BOUND ( 'NONE', #7495, .T. ) ;
#15203=CARTESIAN_POINT ( 'NONE',  ( 1.899999999999999911, 2.000000000000000000, 0.5999999999999999778 ) ) ;
#15218=DIRECTION ( 'NONE',  ( 4.440892098500630106E-16, 0.000000000000000000, -1.000000000000000000 ) ) ;
#15226=EDGE_LOOP ( 'NONE', ( #12997, #10410, #10500, #5210 ) ) ;
#15247=ORIENTED_EDGE ( 'NONE', *, *, #6540, .F. ) ;
#15261=EDGE_CURVE ( 'NONE', #7957, #16569, #15431, .T. ) ;
#15279=ORIENTED_EDGE ( 'NONE', *, *, #2751, .T. ) ;
#15289=VECTOR ( 'NONE', #13813, 1000.000000000000000 ) ;
#15295=VERTEX_POINT ( 'NONE', #18070 ) ;
#15296=FACE_OUTER_BOUND ( 'NONE', #7834, .T. ) ;
#15300=UNCERTAINTY_MEASURE_WITH_UNIT (LENGTH_MEASURE( 1.000000000000000082E-05 ), #1243, 'distance_accuracy_value', 'NONE');
#15301=ORIENTED_EDGE ( 'NONE', *, *, #14374, .T. ) ;
#15346=VECTOR ( 'NONE', #16489, 1000.000000000000000 ) ;
#15379=VERTEX_POINT ( 'NONE', #12541 ) ;
#15397=VERTEX_POINT ( 'NONE', #6044 ) ;
#15421=CARTESIAN_POINT ( 'NONE',  ( 1.899999999999999911, 7.299999999999999822, 1.600000000000000089 ) ) ;
#15431=LINE ( 'NONE', #2737, #16752 ) ;
#15440=CARTESIAN_POINT ( 'NONE',  ( -0.1749999999999999889, 7.700000000000000178, 1.600000000000000089 ) ) ;
#15449=LINE ( 'NONE', #11359, #18215 ) ;
#15464=DIRECTION ( 'NONE',  ( 1.110223024625159992E-16, 0.000000000000000000, -1.000000000000000000 ) ) ;
#15471=DIRECTION ( 'NONE',  ( 0.000000000000000000, 0.000000000000000000, -1.000000000000000000 ) ) ;
#15476=DIRECTION ( 'NONE',  ( 1.000000000000000000, 0.000000000000000000, 1.850371707708589879E-16 ) ) ;
#15477=VERTEX_POINT ( 'NONE', #14562 ) ;
#15479=CARTESIAN_POINT ( 'NONE',  ( -1.899999999999999911, 0.5999999999999999778, 1.600000000000000089 ) ) ;
#15483=CARTESIAN_POINT ( 'NONE',  ( 2.500000000000000000, 2.000000000000000000, 1.600000000000000089 ) ) ;
#15491=FACE_OUTER_BOUND ( 'NONE', #1789, .T. ) ;
#15501=EDGE_CURVE ( 'NONE', #5857, #15295, #8734, .T. ) ;
#15505=ORIENTED_EDGE ( 'NONE', *, *, #17143, .F. ) ;
#15508=EDGE_CURVE ( 'NONE', #10505, #8570, #12821, .T. ) ;
#15517=DIRECTION ( 'NONE',  ( 1.734723475976809806E-16, -1.000000000000000000, -1.387778780781449866E-16 ) ) ;
#15553=LINE ( 'NONE', #4234, #18286 ) ;
#15558=DIRECTION ( 'NONE',  ( -1.708035422500239940E-16, 1.000000000000000000, 8.540177112501209562E-17 ) ) ;
#15564=DIRECTION ( 'NONE',  ( 0.000000000000000000, -1.000000000000000000, -6.167905692361979821E-17 ) ) ;
#15568=AXIS2_PLACEMENT_3D ( 'NONE', #14170, #5559, #7145 ) ;
#15610=CARTESIAN_POINT ( 'NONE',  ( -2.500000000000000000, 7.299999999999999822, 0.5999999999999999778 ) ) ;
#15621=ORIENTED_EDGE ( 'NONE', *, *, #12698, .T. ) ;
#15633=ADVANCED_FACE ( 'NONE', ( #3793 ), #2426, .F. ) ;
#15637=LINE ( 'NONE', #2945, #14419 ) ;
#15662=DIRECTION ( 'NONE',  ( 1.000000000000000000, 0.000000000000000000, 0.000000000000000000 ) ) ;
#15673=ORIENTED_EDGE ( 'NONE', *, *, #14180, .T. ) ;
#15679=CARTESIAN_POINT ( 'NONE',  ( -1.899999999999999911, 10.00000000000000000, 1.600000000000000089 ) ) ;
#15681=DIRECTION ( 'NONE',  ( 1.000000000000000000, 0.000000000000000000, 0.000000000000000000 ) ) ;
#15698=ORIENTED_EDGE ( 'NONE', *, *, #12184, .T. ) ;
#15704=ORIENTED_EDGE ( 'NONE', *, *, #6782, .T. ) ;
#15713=EDGE_CURVE ( 'NONE', #651, #11761, #94, .T. ) ;
#15714=DIRECTION ( 'NONE',  ( 1.000000000000000000, 0.000000000000000000, 0.000000000000000000 ) ) ;
#15732=ADVANCED_FACE ( 'NONE', ( #2867 ), #11201, .T. ) ;
#15750=EDGE_CURVE ( 'NONE', #6294, #16406, #1486, .T. ) ;
#15765=DIRECTION ( 'NONE',  ( 1.110223024625159992E-16, 0.000000000000000000, -1.000000000000000000 ) ) ;
#15821=EDGE_CURVE ( 'NONE', #11761, #8948, #9997, .T. ) ;
#15837=DIRECTION ( 'NONE',  ( -1.908195823574489776E-16, 1.000000000000000000, 0.000000000000000000 ) ) ;
#15838=CARTESIAN_POINT ( 'NONE',  ( 0.1749999999999999889, 5.200000000000000178, 0.5999999999999999778 ) ) ;
#15843=CARTESIAN_POINT ( 'NONE',  ( -1.899999999999999911, 0.5999999999999999778, 0.5999999999999999778 ) ) ;
#15851=DIRECTION ( 'NONE',  ( 0.000000000000000000, -1.000000000000000000, 0.000000000000000000 ) ) ;
#15856=ORIENTED_EDGE ( 'NONE', *, *, #8575, .F. ) ;
#15872=DIRECTION ( 'NONE',  ( 2.220446049250309876E-16, -1.110223024625159992E-16, -1.000000000000000000 ) ) ;
#15901=DIRECTION ( 'NONE',  ( 0.000000000000000000, -1.000000000000000000, 0.000000000000000000 ) ) ;
#15902=DIRECTION ( 'NONE',  ( 0.000000000000000000, -1.000000000000000000, 0.000000000000000000 ) ) ;
#15910=EDGE_LOOP ( 'NONE', ( #4144, #9418, #553, #4880 ) ) ;
#15912=AXIS2_PLACEMENT_3D ( 'NONE', #2976, #9908, #15564 ) ;
#15925=VECTOR ( 'NONE', #12257, 1000.000000000000000 ) ;
#15970=ORIENTED_EDGE ( 'NONE', *, *, #9354, .T. ) ;
#15971=DIRECTION ( 'NONE',  ( 2.220446049250309876E-16, 0.000000000000000000, -1.000000000000000000 ) ) ;
#15977=ORIENTED_EDGE ( 'NONE', *, *, #8461, .T. ) ;
#15987=DIRECTION ( 'NONE',  ( 0.000000000000000000, 1.000000000000000000, 2.775557561562890365E-16 ) ) ;
#15999=DIRECTION ( 'NONE',  ( 0.000000000000000000, 0.000000000000000000, -1.000000000000000000 ) ) ;
#16031=CARTESIAN_POINT ( 'NONE',  ( -0.1749999999999999889, 2.700000000000000178, 0.5999999999999999778 ) ) ;
#16057=ORIENTED_EDGE ( 'NONE', *, *, #9354, .F. ) ;
#16069=CARTESIAN_POINT ( 'NONE',  ( -1.899999999999999911, 11.40000000000000036, 0.5999999999999999778 ) ) ;
#16084=DIRECTION ( 'NONE',  ( -1.000000000000000000, 0.000000000000000000, -1.850371707708589879E-16 ) ) ;
#16088=LINE ( 'NONE', #2098, #5890 ) ;
#16101=VERTEX_POINT ( 'NONE', #12294 ) ;
#16114=DIRECTION ( 'NONE',  ( -1.000000000000000000, 0.000000000000000000, 0.000000000000000000 ) ) ;
#16116=ORIENTED_EDGE ( 'NONE', *, *, #14374, .F. ) ;
#16130=ORIENTED_EDGE ( 'NONE', *, *, #1797, .F. ) ;
#16145=VERTEX_POINT ( 'NONE', #11082 ) ;
#16156=PLANE ( 'NONE',  #2596 ) ;
#16157=FACE_OUTER_BOUND ( 'NONE', #3476, .T. ) ;
#16174=VECTOR ( 'NONE', #17204, 1000.000000000000000 ) ;
#16180=VECTOR ( 'NONE', #3988, 1000.000000000000000 ) ;
#16192=PLANE ( 'NONE',  #11071 ) ;
#16211=ORIENTED_EDGE ( 'NONE', *, *, #13850, .F. ) ;
#16216=ORIENTED_EDGE ( 'NONE', *, *, #15501, .F. ) ;
#16236=DIRECTION ( 'NONE',  ( 3.172065784643300034E-16, -1.000000000000000000, -1.586032892321649771E-16 ) ) ;
#16264=DIRECTION ( 'NONE',  ( -1.000000000000000000, 0.000000000000000000, 0.000000000000000000 ) ) ;
#16282=EDGE_CURVE ( 'NONE', #17446, #1300, #71, .T. ) ;
#16286=ORIENTED_EDGE ( 'NONE', *, *, #8822, .T. ) ;
#16295=EDGE_CURVE ( 'NONE', #6842, #13656, #16725, .T. ) ;
#16319=LINE ( 'NONE', #2442, #18229 ) ;
#16330=EDGE_LOOP ( 'NONE', ( #1626, #13416, #13784, #11804 ) ) ;
#16369=ORIENTED_EDGE ( 'NONE', *, *, #13107, .T. ) ;
#16382=VERTEX_POINT ( 'NONE', #13188 ) ;
#16385=LINE ( 'NONE', #16474, #7626 ) ;
#16405=EDGE_CURVE ( 'NONE', #12255, #5954, #13020, .T. ) ;
#16406=VERTEX_POINT ( 'NONE', #16069 ) ;
#16434=FACE_OUTER_BOUND ( 'NONE', #16330, .T. ) ;
#16439=DIRECTION ( 'NONE',  ( 0.000000000000000000, 0.000000000000000000, -1.000000000000000000 ) ) ;
#16440=LINE ( 'NONE', #14970, #13628 ) ;
#16462=VECTOR ( 'NONE', #7421, 1000.000000000000000 ) ;
#16471=VECTOR ( 'NONE', #1726, 1000.000000000000000 ) ;
#16474=CARTESIAN_POINT ( 'NONE',  ( 2.500000000000000000, 7.299999999999999822, 1.600000000000000089 ) ) ;
#16489=DIRECTION ( 'NONE',  ( 0.000000000000000000, 1.000000000000000000, 0.000000000000000000 ) ) ;
#16492=DIRECTION ( 'NONE',  ( 0.000000000000000000, 0.000000000000000000, -1.000000000000000000 ) ) ;
#16499=DIRECTION ( 'NONE',  ( 1.110223024625159992E-16, 0.000000000000000000, -1.000000000000000000 ) ) ;
#16509=VECTOR ( 'NONE', #10665, 1000.000000000000000 ) ;
#16513=EDGE_CURVE ( 'NONE', #8948, #5954, #9292, .T. ) ;
#16522=SHAPE_REPRESENTATION_RELATIONSHIP ( 'NONE' , 'NONE' ,  #5932, #7745 ) ;
#16525=EDGE_LOOP ( 'NONE', ( #16116, #7133, #2610, #15279 ) ) ;
#16541=CARTESIAN_POINT ( 'NONE',  ( -0.1749999999999999889, 6.799999999999999822, 1.600000000000000089 ) ) ;
#16569=VERTEX_POINT ( 'NONE', #3551 ) ;
#16579=LINE ( 'NONE', #5178, #5865 ) ;
#16581=CARTESIAN_POINT ( 'NONE',  ( -0.1749999999999999889, 4.299999999999999822, 1.600000000000000089 ) ) ;
#16602=EDGE_CURVE ( 'NONE', #9670, #8456, #4941, .T. ) ;
#16609=VERTEX_POINT ( 'NONE', #8022 ) ;
#16613=( NAMED_UNIT ( * ) SI_UNIT ( $, .STERADIAN. ) SOLID_ANGLE_UNIT ( ) );
#16616=ORIENTED_EDGE ( 'NONE', *, *, #14001, .T. ) ;
#16645=LINE ( 'NONE', #18283, #10274 ) ;
#16648=CARTESIAN_POINT ( 'NONE',  ( -2.500000000000000000, 2.000000000000000000, 0.5999999999999999778 ) ) ;
#16671=DIRECTION ( 'NONE',  ( -1.000000000000000000, 0.000000000000000000, 0.000000000000000000 ) ) ;
#16674=DIRECTION ( 'NONE',  ( 0.000000000000000000, -1.000000000000000000, 0.000000000000000000 ) ) ;
#16677=ORIENTED_EDGE ( 'NONE', *, *, #15713, .T. ) ;
#16688=CARTESIAN_POINT ( 'NONE',  ( -2.500000000000000000, 10.00000000000000000, 1.600000000000000089 ) ) ;
#16690=VERTEX_POINT ( 'NONE', #18260 ) ;
#16719=ORIENTED_EDGE ( 'NONE', *, *, #17100, .T. ) ;
#16725=LINE ( 'NONE', #9603, #16765 ) ;
#16735=EDGE_CURVE ( 'NONE', #2376, #17417, #9581, .T. ) ;
#16752=VECTOR ( 'NONE', #15517, 1000.000000000000000 ) ;
#16761=VERTEX_POINT ( 'NONE', #18156 ) ;
#16765=VECTOR ( 'NONE', #12477, 1000.000000000000000 ) ;
#16805=VECTOR ( 'NONE', #5928, 1000.000000000000000 ) ;
#16836=DIRECTION ( 'NONE',  ( 0.000000000000000000, 0.000000000000000000, 1.000000000000000000 ) ) ;
#16852=FACE_BOUND ( 'NONE', #10338, .T. ) ;
#16868=EDGE_CURVE ( 'NONE', #8419, #9933, #14215, .T. ) ;
#16877=DIRECTION ( 'NONE',  ( 1.000000000000000000, 0.000000000000000000, 0.000000000000000000 ) ) ;
#16881=ORIENTED_EDGE ( 'NONE', *, *, #15261, .T. ) ;
#16894=CARTESIAN_POINT ( 'NONE',  ( 1.899999999999999911, 0.5999999999999999778, 0.5999999999999999778 ) ) ;
#16942=ORIENTED_EDGE ( 'NONE', *, *, #14700, .T. ) ;
#16945=ORIENTED_EDGE ( 'NONE', *, *, #9255, .T. ) ;
#16960=CARTESIAN_POINT ( 'NONE',  ( -0.1749999999999999889, 2.700000000000000178, 1.600000000000000089 ) ) ;
#16966=EDGE_LOOP ( 'NONE', ( #4484, #9782, #5471, #12566 ) ) ;
#16968=ORIENTED_EDGE ( 'NONE', *, *, #15821, .F. ) ;
#16971=ORIENTED_EDGE ( 'NONE', *, *, #4537, .F. ) ;
#16975=CARTESIAN_POINT ( 'NONE',  ( -0.1749999999999999889, 5.200000000000000178, 1.600000000000000089 ) ) ;
#16992=DIRECTION ( 'NONE',  ( -1.000000000000000000, -1.734723475976809806E-16, -1.110223024625159992E-16 ) ) ;
#17008=CARTESIAN_POINT ( 'NONE',  ( 1.899999999999999911, 2.000000000000000000, 1.600000000000000089 ) ) ;
#17015=DIRECTION ( 'NONE',  ( 1.000000000000000000, 0.000000000000000000, 0.000000000000000000 ) ) ;
#17026=CARTESIAN_POINT ( 'NONE',  ( -2.500000000000000000, 2.000000000000000000, 0.5999999999999999778 ) ) ;
#17031=CARTESIAN_POINT ( 'NONE',  ( -1.899999999999999911, 2.799999999999999822, 1.600000000000000089 ) ) ;
#17034=PLANE ( 'NONE',  #511 ) ;
#17040=ADVANCED_FACE ( 'NONE', ( #10497 ), #16156, .T. ) ;
#17085=EDGE_LOOP ( 'NONE', ( #9734, #4609, #3185, #9023 ) ) ;
#17086=AXIS2_PLACEMENT_3D ( 'NONE', #8097, #13737, #6795 ) ;
#17099=EDGE_LOOP ( 'NONE', ( #14978, #17134, #9683, #3398 ) ) ;
#17100=EDGE_CURVE ( 'NONE', #15477, #18021, #2080, .T. ) ;
#17123=ADVANCED_FACE ( 'NONE', ( #15155 ), #979, .T. ) ;
#17132=ADVANCED_FACE ( 'NONE', ( #6328 ), #3646, .T. ) ;
#17134=ORIENTED_EDGE ( 'NONE', *, *, #2682, .T. ) ;
#17143=EDGE_CURVE ( 'NONE', #17417, #8570, #11992, .T. ) ;
#17159=EDGE_CURVE ( 'NONE', #2376, #10505, #4945, .T. ) ;
#17168=ADVANCED_FACE ( 'NONE', ( #16434 ), #9402, .T. ) ;
#17204=DIRECTION ( 'NONE',  ( -3.172065784643300034E-16, 1.000000000000000000, 0.000000000000000000 ) ) ;
#17205=CARTESIAN_POINT ( 'NONE',  ( -2.220446049250309876E-16, -9.868649107779171166E-17, 1.600000000000000089 ) ) ;
#17247=CARTESIAN_POINT ( 'NONE',  ( -0.1749999999999999889, 4.299999999999999822, 1.600000000000000089 ) ) ;
#17265=VERTEX_POINT ( 'NONE', #8199 ) ;
#17267=CARTESIAN_POINT ( 'NONE',  ( 0.1749999999999999889, 5.200000000000000178, 1.600000000000000089 ) ) ;
#17276=CARTESIAN_POINT ( 'NONE',  ( 2.500000000000000000, 4.700000000000000178, 0.5999999999999999778 ) ) ;
#17308=VECTOR ( 'NONE', #7160, 1000.000000000000000 ) ;
#17320=CARTESIAN_POINT ( 'NONE',  ( -1.899999999999999911, 2.799999999999999822, 0.5999999999999999778 ) ) ;
#17351=ORIENTED_EDGE ( 'NONE', *, *, #16602, .T. ) ;
#17356=ORIENTED_EDGE ( 'NONE', *, *, #3584, .T. ) ;
#17360=CARTESIAN_POINT ( 'NONE',  ( -1.899999999999999911, 11.40000000000000036, 1.600000000000000089 ) ) ;
#17368=AXIS2_PLACEMENT_3D ( 'NONE', #13715, #16671, #2784 ) ;
#17380=VECTOR ( 'NONE', #9884, 1000.000000000000000 ) ;
#17417=VERTEX_POINT ( 'NONE', #9214 ) ;
#17434=ADVANCED_FACE ( 'NONE', ( #7836 ), #903, .F. ) ;
#17438=CARTESIAN_POINT ( 'NONE',  ( 0.1749999999999999889, 6.799999999999999822, 0.5999999999999999778 ) ) ;
#17442=ORIENTED_EDGE ( 'NONE', *, *, #7481, .T. ) ;
#17446=VERTEX_POINT ( 'NONE', #6541 ) ;
#17468=ORIENTED_EDGE ( 'NONE', *, *, #3500, .F. ) ;
#17470=ORIENTED_EDGE ( 'NONE', *, *, #10395, .T. ) ;
#17473=DIRECTION ( 'NONE',  ( 1.000000000000000000, 0.000000000000000000, 1.168655815394900078E-16 ) ) ;
#17487=EDGE_CURVE ( 'NONE', #4854, #13116, #9121, .T. ) ;
#17492=VERTEX_POINT ( 'NONE', #2287 ) ;
#17555=ORIENTED_EDGE ( 'NONE', *, *, #4151, .F. ) ;
#17559=VECTOR ( 'NONE', #7140, 1000.000000000000000 ) ;
#17578=EDGE_CURVE ( 'NONE', #651, #17998, #9594, .T. ) ;
#17617=ORIENTED_EDGE ( 'NONE', *, *, #17863, .F. ) ;
#17620=DIRECTION ( 'NONE',  ( 0.000000000000000000, 0.000000000000000000, -1.000000000000000000 ) ) ;
#17635=CARTESIAN_POINT ( 'NONE',  ( 2.500000000000000000, 10.00000000000000000, 1.600000000000000089 ) ) ;
#17657=AXIS2_PLACEMENT_3D ( 'NONE', #18077, #5425, #1539 ) ;
#17660=LINE ( 'NONE', #16581, #469 ) ;
#17666=DIRECTION ( 'NONE',  ( 0.000000000000000000, -1.000000000000000000, 0.000000000000000000 ) ) ;
#17675=LINE ( 'NONE', #5015, #14231 ) ;
#17681=AXIS2_PLACEMENT_3D ( 'NONE', #11191, #16836, #4146 ) ;
#17712=CARTESIAN_POINT ( 'NONE',  ( 2.500000000000000000, 9.199999999999999289, 0.5999999999999999778 ) ) ;
#17728=DIRECTION ( 'NONE',  ( -2.220446049250309876E-16, 0.000000000000000000, 1.000000000000000000 ) ) ;
#17729=VERTEX_POINT ( 'NONE', #6232 ) ;
#17752=VECTOR ( 'NONE', #16084, 1000.000000000000000 ) ;
#17786=DIRECTION ( 'NONE',  ( 0.000000000000000000, -1.000000000000000000, 0.000000000000000000 ) ) ;
#17799=ORIENTED_EDGE ( 'NONE', *, *, #4754, .F. ) ;
#17800=LINE ( 'NONE', #5137, #12805 ) ;
#17801=DIRECTION ( 'NONE',  ( -1.000000000000000000, -3.172065784643300034E-16, -2.220446049250309876E-16 ) ) ;
#17805=CARTESIAN_POINT ( 'NONE',  ( 1.899999999999999911, 0.5999999999999999778, 1.600000000000000089 ) ) ;
#17809=EDGE_LOOP ( 'NONE', ( #6466, #8012, #12097, #12470, #1914, #2790, #8723, #1494, #12181, #17617, #2729, #11350, #10597, #5950, #17799, #214, #18044, #2815, #4987, #4343, #7746, #17865, #2522, #15247, #17555, #13458, #9243, #2810 ) ) ;
#17821=ADVANCED_FACE ( 'NONE', ( #4001 ), #962, .T. ) ;
#17833=ORIENTED_EDGE ( 'NONE', *, *, #2363, .T. ) ;
#17839=EDGE_CURVE ( 'NONE', #1588, #8456, #8283, .T. ) ;
#17852=CARTESIAN_POINT ( 'NONE',  ( -1.899999999999999911, 11.40000000000000036, 1.600000000000000089 ) ) ;
#17863=EDGE_CURVE ( 'NONE', #12165, #6842, #10772, .T. ) ;
#17865=ORIENTED_EDGE ( 'NONE', *, *, #9242, .F. ) ;
#17893=CARTESIAN_POINT ( 'NONE',  ( 1.899999999999999911, 2.000000000000000000, 1.600000000000000089 ) ) ;
#17897=VERTEX_POINT ( 'NONE', #9568 ) ;
#17915=DIRECTION ( 'NONE',  ( 1.000000000000000000, 0.000000000000000000, 0.000000000000000000 ) ) ;
#17917=ORIENTED_EDGE ( 'NONE', *, *, #4124, .F. ) ;
#17944=VECTOR ( 'NONE', #862, 1000.000000000000000 ) ;
#17951=EDGE_LOOP ( 'NONE', ( #3261, #1013, #14207, #16369 ) ) ;
#17972=ORIENTED_EDGE ( 'NONE', *, *, #2035, .F. ) ;
#17975=DIRECTION ( 'NONE',  ( 0.000000000000000000, 0.000000000000000000, -1.000000000000000000 ) ) ;
#17980=ORIENTED_EDGE ( 'NONE', *, *, #3500, .T. ) ;
#17990=VERTEX_POINT ( 'NONE', #10193 ) ;
#17998=VERTEX_POINT ( 'NONE', #10034 ) ;
#18010=PLANE ( 'NONE',  #8265 ) ;
#18021=VERTEX_POINT ( 'NONE', #11330 ) ;
#18041=DIRECTION ( 'NONE',  ( 1.110223024625159992E-16, 0.000000000000000000, -1.000000000000000000 ) ) ;
#18044=ORIENTED_EDGE ( 'NONE', *, *, #14920, .F. ) ;
#18051=CARTESIAN_POINT ( 'NONE',  ( 2.500000000000000000, 10.00000000000000000, 0.5999999999999999778 ) ) ;
#18066=EDGE_LOOP ( 'NONE', ( #8175, #945, #9440, #10839 ) ) ;
#18070=CARTESIAN_POINT ( 'NONE',  ( -0.1749999999999999889, 6.799999999999999822, 1.600000000000000089 ) ) ;
#18074=EDGE_CURVE ( 'NONE', #14528, #5861, #1948, .T. ) ;
#18077=CARTESIAN_POINT ( 'NONE',  ( 2.500000000000000000, 7.299999999999999822, 1.600000000000000089 ) ) ;
#18156=CARTESIAN_POINT ( 'NONE',  ( 2.500000000000000000, 4.700000000000000178, 1.600000000000000089 ) ) ;
#18215=VECTOR ( 'NONE', #8400, 1000.000000000000000 ) ;
#18227=DIRECTION ( 'NONE',  ( -0.000000000000000000, 1.000000000000000000, 0.000000000000000000 ) ) ;
#18229=VECTOR ( 'NONE', #15218, 1000.000000000000000 ) ;
#18260=CARTESIAN_POINT ( 'NONE',  ( -0.1749999999999999889, 9.299999999999998934, 1.600000000000000089 ) ) ;
#18278=CARTESIAN_POINT ( 'NONE',  ( 1.899999999999999911, 7.299999999999999822, 1.600000000000000089 ) ) ;
#18283=CARTESIAN_POINT ( 'NONE',  ( 1.899999999999999911, 2.799999999999999822, 0.5999999999999999778 ) ) ;
#18286=VECTOR ( 'NONE', #946, 1000.000000000000000 ) ;
#18289=EDGE_CURVE ( 'NONE', #2568, #10948, #11284, .T. ) ;
#18291=DIRECTION ( 'NONE',  ( 1.168655815394900078E-16, -1.000000000000000000, 0.000000000000000000 ) ) ;
ENDSEC;
END-ISO-10303-21;
